ISO-10303-21;
HEADER;
FILE_DESCRIPTION (('STEP AP214'),
    '1' );
FILE_NAME ('torque nut 08_iso_ISO 10511-M5-N.step',
    '2026-09-30T16:28:02',
    ( '' ),
    ( '' ),
    'SwSTEP 2.0',
    'SolidWorks 2026',
    '' );
FILE_SCHEMA (( 'AUTOMOTIVE_DESIGN' ));
ENDSEC;

DATA;
#26=EDGE_CURVE ( 'NONE', #4351, #19336, #2033, .T. ) ;
#67=ADVANCED_FACE ( 'NONE', ( #10563 ), #23345, .T. ) ;
#116=ORIENTED_EDGE ( 'NONE', *, *, #15748, .F. ) ;
#149=CARTESIAN_POINT ( 'NONE',  ( 2.681483223904240987, -3.070647092368469000, -1.935399088488818784E-14 ) ) ;
#153=CARTESIAN_POINT ( 'NONE',  ( 2.681483223904239210, -3.070647092368469888, -2.449999999999981526 ) ) ;
#159=EDGE_LOOP ( 'NONE', ( #26416, #20903, #28794, #24499, #27382, #1252 ) ) ;
#331=ORIENTED_EDGE ( 'NONE', *, *, #10865, .F. ) ;
#382=CARTESIAN_POINT ( 'NONE',  ( 1.214306433183764966E-14, 4.618802153517016507, -2.092734410091829034 ) ) ;
#397=EDGE_LOOP ( 'NONE', ( #19913, #23499 ) ) ;
#398=CARTESIAN_POINT ( 'NONE',  ( 1.734723475976807094E-15, 2.928571428571426161, 2.549999999999999378 ) ) ;
#404=EDGE_LOOP ( 'NONE', ( #3779, #2242, #2825, #27348 ) ) ;
#409=EDGE_CURVE ( 'NONE', #5044, #29035, #5775, .T. ) ;
#461=VERTEX_POINT ( 'NONE', #21635 ) ;
#462=DIRECTION ( 'NONE',  ( -1.000000000000000000, -4.440892098500623203E-16, 0.000000000000000000 ) ) ;
#474=CARTESIAN_POINT ( 'NONE',  ( -4.000000000000010658, -2.309401076758525573, -0.3572655899081716435 ) ) ;
#497=CARTESIAN_POINT ( 'NONE',  ( -2.500000000000002665, -1.110223024625156738E-15, -2.424599999999998978 ) ) ;
#501=DIRECTION ( 'NONE',  ( -1.000000000000000000, -4.440892098500622217E-16, 0.000000000000000000 ) ) ;
#502=CIRCLE ( 'NONE', #23914, 4.000000000000003553 ) ;
#565=AXIS2_PLACEMENT_3D ( 'NONE', #8777, #15341, #10624 ) ;
#682=FACE_BOUND ( 'NONE', #6347, .T. ) ;
#691=CARTESIAN_POINT ( 'NONE',  ( -1.321505333908961966, 3.855830693249140406, -2.415789719053470730 ) ) ;
#694=CARTESIAN_POINT ( 'NONE',  ( 3.673643420401897508, 2.497823135841249709, -2.201519936625011553 ) ) ;
#703=AXIS2_PLACEMENT_3D ( 'NONE', #17964, #20256, #19964 ) ;
#714=CARTESIAN_POINT ( 'NONE',  ( -4.000000000000005329, 0.7862748000878123644, -2.415527722372433406 ) ) ;
#736=ORIENTED_EDGE ( 'NONE', *, *, #27325, .F. ) ;
#781=AXIS2_PLACEMENT_3D ( 'NONE', #25947, #14624, #462 ) ;
#783=EDGE_CURVE ( 'NONE', #2732, #4135, #16160, .T. ) ;
#786=CIRCLE ( 'NONE', #8089, 4.000000000000004441 ) ;
#815=EDGE_CURVE ( 'NONE', #4780, #461, #13982, .T. ) ;
#906=CIRCLE ( 'NONE', #8193, 4.000000000000003553 ) ;
#952=VERTEX_POINT ( 'NONE', #1434 ) ;
#958=ORIENTED_EDGE ( 'NONE', *, *, #11692, .F. ) ;
#974=CARTESIAN_POINT ( 'NONE',  ( 0.000000000000000000, 0.000000000000000000, 1.700000000000000178 ) ) ;
#986=AXIS2_PLACEMENT_3D ( 'NONE', #29053, #17398, #15258 ) ;
#1041=DIRECTION ( 'NONE',  ( 1.000000000000000000, 4.440892098500622217E-16, 0.000000000000000000 ) ) ;
#1057=DIRECTION ( 'NONE',  ( 1.000000000000000000, 4.440892098500622217E-16, 0.000000000000000000 ) ) ;
#1118=( NAMED_UNIT ( * ) PLANE_ANGLE_UNIT ( ) SI_UNIT ( $, .RADIAN. ) );
#1129=DIRECTION ( 'NONE',  ( 1.000000000000000000, 4.440892098500622217E-16, 0.000000000000000000 ) ) ;
#1168=EDGE_CURVE ( 'NONE', #13842, #18112, #10665, .T. ) ;
#1183=PLANE ( 'NONE',  #10266 ) ;
#1252=ORIENTED_EDGE ( 'NONE', *, *, #2182, .F. ) ;
#1289=CONICAL_SURFACE ( 'NONE', #16877, 4.000000000000003553, 1.047197551196597853 ) ;
#1293=DIRECTION ( 'NONE',  ( 1.000000000000000000, 4.440892098500622217E-16, 0.000000000000000000 ) ) ;
#1297=DIRECTION ( 'NONE',  ( 1.000000000000000000, 4.440892098500622217E-16, 0.000000000000000000 ) ) ;
#1357=CONICAL_SURFACE ( 'NONE', #21798, 4.000000000000003553, 1.047197551196597853 ) ;
#1374=ORIENTED_EDGE ( 'NONE', *, *, #5125, .F. ) ;
#1432=ORIENTED_EDGE ( 'NONE', *, *, #6569, .F. ) ;
#1434=CARTESIAN_POINT ( 'NONE',  ( 2.000000000000003553, -3.464101615137736623, 8.673617379884035472E-16 ) ) ;
#1545=AXIS2_PLACEMENT_3D ( 'NONE', #18091, #15948, #15655 ) ;
#1607=CARTESIAN_POINT ( 'NONE',  ( -4.000000000000004441, -1.549102112939102271, -2.292104661404058774 ) ) ;
#1651=CONICAL_SURFACE ( 'NONE', #6535, 4.000000000000003553, 1.047197551196597853 ) ;
#1680=ORIENTED_EDGE ( 'NONE', *, *, #15410, .T. ) ;
#1690=CARTESIAN_POINT ( 'NONE',  ( 2.000000000000008882, -3.464101615137750390, -2.450000000000000622 ) ) ;
#1729=( LENGTH_UNIT ( ) NAMED_UNIT ( * ) SI_UNIT ( .MILLI., .METRE. ) );
#1809=B_SPLINE_CURVE_WITH_KNOTS ( 'NONE', 3,
 ( #27957, #21045, #149, #11329 ),
 .UNSPECIFIED., .F., .F.,
 ( 4, 4 ),
 ( 2.380737581964344716E-07, 0.002336974151641508721 ),
 .UNSPECIFIED. ) ;
#1882=ORIENTED_EDGE ( 'NONE', *, *, #18338, .T. ) ;
#1886=SHAPE_REPRESENTATION_RELATIONSHIP ( 'NONE' , 'NONE' ,  #6235, #6562 ) ;
#1888=AXIS2_PLACEMENT_3D ( 'NONE', #23992, #18290, #13572 ) ;
#1912=ORIENTED_EDGE ( 'NONE', *, *, #7771, .F. ) ;
#1916=CARTESIAN_POINT ( 'NONE',  ( -4.000000000000004441, -0.3902508023145583871, -2.693564772268675078E-15 ) ) ;
#1933=DIRECTION ( 'NONE',  ( 0.000000000000000000, 0.000000000000000000, 1.000000000000000000 ) ) ;
#1965=( GEOMETRIC_REPRESENTATION_CONTEXT ( 3 ) GLOBAL_UNCERTAINTY_ASSIGNED_CONTEXT ( ( #18347 ) ) GLOBAL_UNIT_ASSIGNED_CONTEXT ( ( #28940, #29705, #22935 ) ) REPRESENTATION_CONTEXT ( 'NONE', 'WORKASPACE' ) );
#1972=ADVANCED_FACE ( 'NONE', ( #2081 ), #11215, .T. ) ;
#2033=B_SPLINE_CURVE_WITH_KNOTS ( 'NONE', 3,
 ( #24314, #22164, #29550, #17867, #29234, #27083 ),
 .UNSPECIFIED., .F., .F.,
 ( 4, 2, 4 ),
 ( 0.006456566858647387087, 0.007625406818786638688, 0.008794246778925891156 ),
 .UNSPECIFIED. ) ;
#2081=FACE_OUTER_BOUND ( 'NONE', #21700, .T. ) ;
#2111=EDGE_CURVE ( 'NONE', #18112, #26865, #786, .T. ) ;
#2123=CARTESIAN_POINT ( 'NONE',  ( 1.214306433183764966E-14, 4.618802153517016507, -2.450000000000000178 ) ) ;
#2151=AXIS2_PLACEMENT_3D ( 'NONE', #28036, #4349, #7090 ) ;
#2169=DIRECTION ( 'NONE',  ( 0.000000000000000000, 0.000000000000000000, 1.000000000000000000 ) ) ;
#2180=DIRECTION ( 'NONE',  ( 1.000000000000000000, 4.440892098500621724E-16, 0.000000000000000000 ) ) ;
#2182=EDGE_CURVE ( 'NONE', #461, #12786, #3042, .T. ) ;
#2242=ORIENTED_EDGE ( 'NONE', *, *, #20926, .F. ) ;
#2258=CIRCLE ( 'NONE', #19286, 4.000000000000003553 ) ;
#2302=CARTESIAN_POINT ( 'NONE',  ( -2.681483223904239210, 3.070647092368423259, 4.157051104216616720E-15 ) ) ;
#2311=ORIENTED_EDGE ( 'NONE', *, *, #20926, .T. ) ;
#2325=CARTESIAN_POINT ( 'NONE',  ( -7.806255641895631925E-14, -4.618802153517044928, -2.092734410091829034 ) ) ;
#2328=CARTESIAN_POINT ( 'NONE',  ( -2.339468227445740123, -3.268109542640673215, -2.121182258161580993E-14 ) ) ;
#2335=CARTESIAN_POINT ( 'NONE',  ( 3.999999999999996447, 0.000000000000000000, 8.673617379884035472E-16 ) ) ;
#2394=DIRECTION ( 'NONE',  ( -0.000000000000000000, -0.000000000000000000, 1.000000000000000000 ) ) ;
#2451=ORIENTED_EDGE ( 'NONE', *, *, #24144, .F. ) ;
#2479=CARTESIAN_POINT ( 'NONE',  ( -2.000000000000032863, -3.464101615137743728, 8.673617379884035472E-16 ) ) ;
#2621=CARTESIAN_POINT ( 'NONE',  ( 2.000000000000008882, -3.464101615137750390, -2.450000000000000622 ) ) ;
#2672=CARTESIAN_POINT ( 'NONE',  ( 0.000000000000000000, 2.099999999999997868, 1.700000000000000178 ) ) ;
#2709=AXIS2_PLACEMENT_3D ( 'NONE', #6808, #2394, #20675 ) ;
#2732=VERTEX_POINT ( 'NONE', #27700 ) ;
#2756=DIRECTION ( 'NONE',  ( -1.000000000000000000, -4.440892098500622217E-16, 0.000000000000000000 ) ) ;
#2789=DIRECTION ( 'NONE',  ( -0.8191520442889902442, -3.637765840953607804E-16, -0.5735764363510482688 ) ) ;
#2795=UNCERTAINTY_MEASURE_WITH_UNIT (LENGTH_MEASURE( 1.000000000000000082E-05 ), #28013, 'distance_accuracy_value', 'NONE');
#2825=ORIENTED_EDGE ( 'NONE', *, *, #5895, .T. ) ;
#2829=CARTESIAN_POINT ( 'NONE',  ( 2.000000000000026201, 3.464101615137736623, -2.450000000000000622 ) ) ;
#2856=CIRCLE ( 'NONE', #14517, 4.000000000000000000 ) ;
#2876=ORIENTED_EDGE ( 'NONE', *, *, #5634, .F. ) ;
#2888=AXIS2_PLACEMENT_3D ( 'NONE', #6881, #16169, #25492 ) ;
#2904=CARTESIAN_POINT ( 'NONE',  ( -2.000000000000008882, 3.464101615137750390, 0.000000000000000000 ) ) ;
#2916=ORIENTED_EDGE ( 'NONE', *, *, #8493, .F. ) ;
#2918=DIRECTION ( 'NONE',  ( 1.000000000000000000, 4.440892098500622217E-16, 0.000000000000000000 ) ) ;
#2970=CIRCLE ( 'NONE', #10229, 3.150000000000000799 ) ;
#3042=B_SPLINE_CURVE_WITH_KNOTS ( 'NONE', 3,
 ( #382, #26026, #23731, #2829 ),
 .UNSPECIFIED., .F., .F.,
 ( 4, 4 ),
 ( 2.380737581676944055E-07, 0.002336974151641584615 ),
 .UNSPECIFIED. ) ;
#3046=DIRECTION ( 'NONE',  ( 0.000000000000000000, 0.000000000000000000, 1.000000000000000000 ) ) ;
#3072=EDGE_CURVE ( 'NONE', #29919, #26117, #21869, .T. ) ;
#3077=EDGE_CURVE ( 'NONE', #9008, #21764, #23325, .T. ) ;
#3237=ORIENTED_EDGE ( 'NONE', *, *, #29958, .F. ) ;
#3243=CYLINDRICAL_SURFACE ( 'NONE', #13074, 2.928571428571432378 ) ;
#3410=ORIENTED_EDGE ( 'NONE', *, *, #21711, .T. ) ;
#3416=( GEOMETRIC_REPRESENTATION_CONTEXT ( 3 ) GLOBAL_UNCERTAINTY_ASSIGNED_CONTEXT ( ( #13762 ) ) GLOBAL_UNIT_ASSIGNED_CONTEXT ( ( #1729, #8569, #3709 ) ) REPRESENTATION_CONTEXT ( 'NONE', 'WORKASPACE' ) );
#3461=CARTESIAN_POINT ( 'NONE',  ( 4.000000000000010658, -2.309401076758560656, -2.450000000000000178 ) ) ;
#3560=CARTESIAN_POINT ( 'NONE',  ( -3.149999999999999023, -1.013117269296279552E-15, 1.700000000000000178 ) ) ;
#3567=DIRECTION ( 'NONE',  ( 0.8660254037844369313, 0.5000000000000028866, 0.000000000000000000 ) ) ;
#3587=ORIENTED_EDGE ( 'NONE', *, *, #14990, .T. ) ;
#3600=EDGE_CURVE ( 'NONE', #22117, #3702, #24404, .T. ) ;
#3606=DIRECTION ( 'NONE',  ( 0.5000000000000066613, 0.8660254037844349329, 0.000000000000000000 ) ) ;
#3617=CONICAL_SURFACE ( 'NONE', #7984, 4.000000000000003553, 1.047197551196597853 ) ;
#3702=VERTEX_POINT ( 'NONE', #28960 ) ;
#3709=( NAMED_UNIT ( * ) SI_UNIT ( $, .STERADIAN. ) SOLID_ANGLE_UNIT ( ) );
#3714=ORIENTED_EDGE ( 'NONE', *, *, #815, .F. ) ;
#3733=CARTESIAN_POINT ( 'NONE',  ( -4.000000000000003553, -0.7779732554280821555, -2.416455648918319987 ) ) ;
#3742=CARTESIAN_POINT ( 'NONE',  ( 0.000000000000000000, 0.000000000000000000, -2.450000000000000622 ) ) ;
#3766=CARTESIAN_POINT ( 'NONE',  ( -7.806255641895631925E-14, -4.618802153517044928, -0.3572655899081716435 ) ) ;
#3779=ORIENTED_EDGE ( 'NONE', *, *, #7162, .F. ) ;
#3872=CIRCLE ( 'NONE', #20913, 2.928571428571432378 ) ;
#3938=DIRECTION ( 'NONE',  ( -1.000000000000000000, -4.440892098500622217E-16, 0.000000000000000000 ) ) ;
#3940=DIRECTION ( 'NONE',  ( 0.000000000000000000, 0.000000000000000000, 1.000000000000000000 ) ) ;
#3943=ORIENTED_EDGE ( 'NONE', *, *, #23889, .F. ) ;
#3965=DIRECTION ( 'NONE',  ( 0.000000000000000000, 0.000000000000000000, 1.000000000000000000 ) ) ;
#4007=SURFACE_STYLE_FILL_AREA ( #8425 ) ;
#4021=EDGE_CURVE ( 'NONE', #28630, #14061, #9112, .T. ) ;
#4028=ORIENTED_EDGE ( 'NONE', *, *, #21000, .F. ) ;
#4130=ORIENTED_EDGE ( 'NONE', *, *, #10025, .F. ) ;
#4135=VERTEX_POINT ( 'NONE', #27942 ) ;
#4201=CARTESIAN_POINT ( 'NONE',  ( -3.673643420401920601, -2.497823135841290565, -2.201519936624986240 ) ) ;
#4212=CARTESIAN_POINT ( 'NONE',  ( 1.321505333908962632, -3.855830693249187480, -0.03421028094655551716 ) ) ;
#4243=CIRCLE ( 'NONE', #21291, 3.150000000000000799 ) ;
#4349=DIRECTION ( 'NONE',  ( 0.000000000000000000, 0.000000000000000000, 1.000000000000000000 ) ) ;
#4351=VERTEX_POINT ( 'NONE', #14746 ) ;
#4354=DIRECTION ( 'NONE',  ( 0.000000000000000000, 0.000000000000000000, 1.000000000000000000 ) ) ;
#4377=ORIENTED_EDGE ( 'NONE', *, *, #19365, .F. ) ;
#4379=ORIENTED_EDGE ( 'NONE', *, *, #24144, .T. ) ;
#4433=ORIENTED_EDGE ( 'NONE', *, *, #19029, .T. ) ;
#4447=LINE ( 'NONE', #18171, #22289 ) ;
#4476=DIRECTION ( 'NONE',  ( -0.000000000000000000, -0.000000000000000000, 1.000000000000000000 ) ) ;
#4487=VERTEX_POINT ( 'NONE', #22698 ) ;
#4494=CARTESIAN_POINT ( 'NONE',  ( 4.000000000000000000, -0.3902508023145602190, 3.244136187983970792E-16 ) ) ;
#4542=LINE ( 'NONE', #13831, #19695 ) ;
#4543=CARTESIAN_POINT ( 'NONE',  ( -4.000000000000010658, -2.309401076758525573, -0.3572655899081716435 ) ) ;
#4625=PRESENTATION_STYLE_ASSIGNMENT (( #7668 ) ) ;
#4627=ORIENTED_EDGE ( 'NONE', *, *, #5634, .T. ) ;
#4639=CARTESIAN_POINT ( 'NONE',  ( 4.000000000000000000, -1.549102112939128917, -0.1578953385959452616 ) ) ;
#4667=PRODUCT_DEFINITION ( 'UNKNOWN', '', #11199, #27855 ) ;
#4731=ORIENTED_EDGE ( 'NONE', *, *, #18338, .F. ) ;
#4766=ORIENTED_EDGE ( 'NONE', *, *, #5848, .F. ) ;
#4780=VERTEX_POINT ( 'NONE', #14882 ) ;
#4790=CARTESIAN_POINT ( 'NONE',  ( 4.000000000000000000, -1.933795701539638534, -0.2488376576623040348 ) ) ;
#4795=VECTOR ( 'NONE', #3965, 1000.000000000000000 ) ;
#4813=ADVANCED_FACE ( 'NONE', ( #22080 ), #1183, .F. ) ;
#4838=CONICAL_SURFACE ( 'NONE', #26791, 4.000000000000003553, 1.047197551196597853 ) ;
#4850=CARTESIAN_POINT ( 'NONE',  ( 0.000000000000000000, 0.000000000000000000, 2.550000000000000266 ) ) ;
#4890=CARTESIAN_POINT ( 'NONE',  ( 0.3263565795980564732, -4.430380094434313243, -2.201519936624962259 ) ) ;
#4910=ADVANCED_FACE ( 'NONE', ( #26840 ), #16889, .F. ) ;
#4927=DIRECTION ( 'NONE',  ( 0.000000000000000000, 0.000000000000000000, 1.000000000000000000 ) ) ;
#4997=B_SPLINE_CURVE_WITH_KNOTS ( 'NONE', 3,
 ( #27875, #25092, #9037, #13331, #6930, #22807 ),
 .UNSPECIFIED., .F., .F.,
 ( 4, 2, 4 ),
 ( 0.004120275011746841846, 0.005288420935197130079, 0.006456566858647419180 ),
 .UNSPECIFIED. ) ;
#5020=CARTESIAN_POINT ( 'NONE',  ( 0.000000000000000000, 0.000000000000000000, -2.450000000000000622 ) ) ;
#5027=ORIENTED_EDGE ( 'NONE', *, *, #11950, .T. ) ;
#5044=VERTEX_POINT ( 'NONE', #13513 ) ;
#5075=SURFACE_SIDE_STYLE ('',( #28611 ) ) ;
#5083=B_SPLINE_CURVE_WITH_KNOTS ( 'NONE', 3,
 ( #10917, #8628, #4212, #8480, #18089, #3766 ),
 .UNSPECIFIED., .F., .F.,
 ( 4, 2, 4 ),
 ( 0.002336974151641508721, 0.003500975885716453660, 0.004664977619791398598 ),
 .UNSPECIFIED. ) ;
#5099=CARTESIAN_POINT ( 'NONE',  ( 0.000000000000000000, 0.000000000000000000, 0.000000000000000000 ) ) ;
#5119=EDGE_CURVE ( 'NONE', #7935, #29938, #6901, .T. ) ;
#5124=ORIENTED_EDGE ( 'NONE', *, *, #10865, .T. ) ;
#5125=EDGE_CURVE ( 'NONE', #28553, #12786, #21496, .T. ) ;
#5137=ORIENTED_EDGE ( 'NONE', *, *, #4021, .T. ) ;
#5204=AXIS2_PLACEMENT_3D ( 'NONE', #24791, #4476, #24945 ) ;
#5232=ORIENTED_EDGE ( 'NONE', *, *, #6569, .T. ) ;
#5283=VECTOR ( 'NONE', #2789, 1000.000000000000114 ) ;
#5339=DIRECTION ( 'NONE',  ( 0.000000000000000000, 0.000000000000000000, -1.000000000000000000 ) ) ;
#5435=CARTESIAN_POINT ( 'NONE',  ( 0.000000000000000000, 0.000000000000000000, 0.000000000000000000 ) ) ;
#5442=B_SPLINE_CURVE_WITH_KNOTS ( 'NONE', 3,
 ( #20566, #13838, #15986, #20708, #16139, #11545 ),
 .UNSPECIFIED., .F., .F.,
 ( 4, 2, 4 ),
 ( 0.002336974151641585049, 0.003500975885716457129, 0.004664977619791329209 ),
 .UNSPECIFIED. ) ;
#5458=CARTESIAN_POINT ( 'NONE',  ( 0.000000000000000000, 0.000000000000000000, 1.700000000000000178 ) ) ;
#5465=EDGE_LOOP ( 'NONE', ( #2451, #5137, #11933, #27372 ) ) ;
#5490=VERTEX_POINT ( 'NONE', #19740 ) ;
#5550=ORIENTED_EDGE ( 'NONE', *, *, #7162, .T. ) ;
#5582=AXIS2_PLACEMENT_3D ( 'NONE', #19319, #28986, #19172 ) ;
#5597=AXIS2_PLACEMENT_3D ( 'NONE', #2672, #16707, #19432 ) ;
#5634=EDGE_CURVE ( 'NONE', #6899, #13842, #10312, .T. ) ;
#5638=ORIENTED_EDGE ( 'NONE', *, *, #21711, .F. ) ;
#5712=DIRECTION ( 'NONE',  ( 1.000000000000000000, 4.440892098500622217E-16, 0.000000000000000000 ) ) ;
#5714=EDGE_CURVE ( 'NONE', #29328, #8506, #9261, .T. ) ;
#5771=CONICAL_SURFACE ( 'NONE', #1888, 4.000000000000003553, 1.047197551196597853 ) ;
#5775=LINE ( 'NONE', #26542, #27276 ) ;
#5776=DIRECTION ( 'NONE',  ( 0.000000000000000000, 0.000000000000000000, 1.000000000000000000 ) ) ;
#5796=CARTESIAN_POINT ( 'NONE',  ( -2.928571428571432378, -9.419004090963157619E-16, 9.480888224575629408 ) ) ;
#5848=EDGE_CURVE ( 'NONE', #27629, #12251, #2970, .T. ) ;
#5850=EDGE_CURVE ( 'NONE', #4487, #18112, #25617, .T. ) ;
#5874=AXIS2_PLACEMENT_3D ( 'NONE', #24794, #10882, #1297 ) ;
#5895=EDGE_CURVE ( 'NONE', #21764, #29919, #25687, .T. ) ;
#5902=FACE_OUTER_BOUND ( 'NONE', #159, .T. ) ;
#5948=LINE ( 'NONE', #5796, #4795 ) ;
#5992=CIRCLE ( 'NONE', #18649, 2.500000000000002665 ) ;
#6020=CARTESIAN_POINT ( 'NONE',  ( -4.000000000000010658, -2.309401076758525573, -2.092734410091829034 ) ) ;
#6134=EDGE_LOOP ( 'NONE', ( #6660, #11581, #9398 ) ) ;
#6215=CARTESIAN_POINT ( 'NONE',  ( -4.000000000000001776, -1.286498119741308097E-15, 9.480888224575629408 ) ) ;
#6235=SHAPE_REPRESENTATION ( 'torque nut 08_iso_ISO 10511-M5-N', ( #13190 ), #1965 ) ;
#6331=CARTESIAN_POINT ( 'NONE',  ( -4.000000000000004441, -1.549102112939100273, -0.1578953385959418754 ) ) ;
#6347=EDGE_LOOP ( 'NONE', ( #29434, #17755 ) ) ;
#6350=DIRECTION ( 'NONE',  ( 0.000000000000000000, 0.000000000000000000, 1.000000000000000000 ) ) ;
#6472=CARTESIAN_POINT ( 'NONE',  ( -4.000000000000003553, -6.938893903907228378E-15, -2.450000000000000178 ) ) ;
#6535=AXIS2_PLACEMENT_3D ( 'NONE', #29412, #8433, #10418 ) ;
#6562=ADVANCED_BREP_SHAPE_REPRESENTATION ( '', ( #11686, #13190 ), #1965 ) ;
#6569=EDGE_CURVE ( 'NONE', #23922, #4780, #9168, .T. ) ;
#6660=ORIENTED_EDGE ( 'NONE', *, *, #815, .T. ) ;
#6667=EDGE_LOOP ( 'NONE', ( #17570, #16992, #19207, #1374, #331, #27010 ) ) ;
#6722=DIRECTION ( 'NONE',  ( -1.000000000000000000, -4.440892098500622217E-16, 0.000000000000000000 ) ) ;
#6808=CARTESIAN_POINT ( 'NONE',  ( 0.000000000000000000, 0.000000000000000000, -2.450000000000000178 ) ) ;
#6831=DIRECTION ( 'NONE',  ( 1.000000000000000000, 4.440892098500622217E-16, 0.000000000000000000 ) ) ;
#6857=DIRECTION ( 'NONE',  ( 0.000000000000000000, 0.000000000000000000, 1.000000000000000000 ) ) ;
#6860=DIRECTION ( 'NONE',  ( 0.000000000000000000, 0.000000000000000000, 1.000000000000000000 ) ) ;
#6881=CARTESIAN_POINT ( 'NONE',  ( 0.000000000000000000, 0.000000000000000000, -2.144516984716112518 ) ) ;
#6899=VERTEX_POINT ( 'NONE', #11974 ) ;
#6901=CIRCLE ( 'NONE', #1545, 2.928571428571432378 ) ;
#6921=VERTEX_POINT ( 'NONE', #20834 ) ;
#6930=CARTESIAN_POINT ( 'NONE',  ( 4.000000000000000000, -0.3902508023145602190, -2.450000000000001066 ) ) ;
#6998=ORIENTED_EDGE ( 'NONE', *, *, #24395, .T. ) ;
#7037=AXIS2_PLACEMENT_3D ( 'NONE', #2123, #14279, #30237 ) ;
#7090=DIRECTION ( 'NONE',  ( 1.000000000000000000, 4.440892098500622217E-16, 0.000000000000000000 ) ) ;
#7162=EDGE_CURVE ( 'NONE', #9008, #26117, #26653, .T. ) ;
#7189=CARTESIAN_POINT ( 'NONE',  ( 1.660531772554315610, -3.660093687634890181, -2.449999999999980194 ) ) ;
#7192=ORIENTED_EDGE ( 'NONE', *, *, #4021, .F. ) ;
#7208=ORIENTED_EDGE ( 'NONE', *, *, #9204, .T. ) ;
#7225=CARTESIAN_POINT ( 'NONE',  ( 2.100000000000000977, 9.325873406851313362E-16, -2.450000000000000178 ) ) ;
#7252=CARTESIAN_POINT ( 'NONE',  ( 4.000000000000001776, 1.776356839400249676E-15, 9.480888224575629408 ) ) ;
#7278=AXIS2_PLACEMENT_3D ( 'NONE', #974, #29399, #1129 ) ;
#7296=CARTESIAN_POINT ( 'NONE',  ( 3.999999999999999112, 0.7862748000878193588, -2.415527722372434738 ) ) ;
#7320=EDGE_CURVE ( 'NONE', #9337, #4351, #25890, .T. ) ;
#7465=B_SPLINE_CURVE_WITH_KNOTS ( 'NONE', 3,
 ( #11349, #4790, #4639, #16076, #4494, #14080 ),
 .UNSPECIFIED., .F., .F.,
 ( 4, 2, 4 ),
 ( 0.004120275011746841846, 0.005288420935197130079, 0.006456566858647419180 ),
 .UNSPECIFIED. ) ;
#7468=DIRECTION ( 'NONE',  ( 0.000000000000000000, 0.000000000000000000, 1.000000000000000000 ) ) ;
#7485=CARTESIAN_POINT ( 'NONE',  ( -2.678494666091076226, -3.072372537026388351, -0.03421028094655393509 ) ) ;
#7522=EDGE_LOOP ( 'NONE', ( #5232, #10645, #14926 ) ) ;
#7542=DIRECTION ( 'NONE',  ( -1.000000000000000000, -4.440892098500622217E-16, 0.000000000000000000 ) ) ;
#7555=AXIS2_PLACEMENT_3D ( 'NONE', #10082, #26442, #14210 ) ;
#7573=EDGE_CURVE ( 'NONE', #18112, #6899, #15321, .T. ) ;
#7589=CARTESIAN_POINT ( 'NONE',  ( 4.000000000000000000, 1.557668341133518819, -2.290303434304245211 ) ) ;
#7668=SURFACE_STYLE_USAGE ( .BOTH. , #5075 ) ;
#7708=ADVANCED_FACE ( 'NONE', ( #20967 ), #13644, .T. ) ;
#7734=DIRECTION ( 'NONE',  ( 0.000000000000000000, 0.000000000000000000, 1.000000000000000000 ) ) ;
#7771=EDGE_CURVE ( 'NONE', #5490, #952, #19988, .T. ) ;
#7809=AXIS2_PLACEMENT_3D ( 'NONE', #5099, #17147, #7542 ) ;
#7852=CARTESIAN_POINT ( 'NONE',  ( -0.6554360035617876612, 4.240386000424035906, -0.1586754815284892317 ) ) ;
#7935=VERTEX_POINT ( 'NONE', #21120 ) ;
#7947=LINE ( 'NONE', #497, #5283 ) ;
#7971=EDGE_LOOP ( 'NONE', ( #3587, #21904, #24806 ) ) ;
#7984=AXIS2_PLACEMENT_3D ( 'NONE', #5020, #7468, #22636 ) ;
#8089=AXIS2_PLACEMENT_3D ( 'NONE', #30199, #11657, #12113 ) ;
#8090=ORIENTED_EDGE ( 'NONE', *, *, #12799, .F. ) ;
#8093=FACE_OUTER_BOUND ( 'NONE', #17562, .T. ) ;
#8103=VERTEX_POINT ( 'NONE', #8276 ) ;
#8110=ADVANCED_FACE ( 'NONE', ( #10416 ), #22485, .T. ) ;
#8193=AXIS2_PLACEMENT_3D ( 'NONE', #14601, #3046, #1057 ) ;
#8243=ORIENTED_EDGE ( 'NONE', *, *, #12552, .T. ) ;
#8276=CARTESIAN_POINT ( 'NONE',  ( -2.928571428571429713, -9.419004090963149730E-16, 1.700000000000000178 ) ) ;
#8340=CARTESIAN_POINT ( 'NONE',  ( 0.000000000000000000, 0.000000000000000000, -2.450000000000000178 ) ) ;
#8425=FILL_AREA_STYLE ('',( #20473 ) ) ;
#8433=DIRECTION ( 'NONE',  ( 0.000000000000000000, 0.000000000000000000, -1.000000000000000000 ) ) ;
#8437=CONICAL_SURFACE ( 'NONE', #2151, 4.000000000000003553, 1.047197551196597853 ) ;
#8454=CARTESIAN_POINT ( 'NONE',  ( -4.000000000000003553, -0.7779732554280804901, -0.03354435108168069002 ) ) ;
#8480=CARTESIAN_POINT ( 'NONE',  ( 0.6554360035617698976, -4.240386000424092749, -0.1586754815285197906 ) ) ;
#8489=ORIENTED_EDGE ( 'NONE', *, *, #5119, .T. ) ;
#8493=EDGE_CURVE ( 'NONE', #4135, #18869, #15652, .T. ) ;
#8506=VERTEX_POINT ( 'NONE', #20141 ) ;
#8569=( NAMED_UNIT ( * ) PLANE_ANGLE_UNIT ( ) SI_UNIT ( $, .RADIAN. ) );
#8572=ORIENTED_EDGE ( 'NONE', *, *, #1168, .T. ) ;
#8600=DIRECTION ( 'NONE',  ( 0.000000000000000000, 0.000000000000000000, -1.000000000000000000 ) ) ;
#8622=( GEOMETRIC_REPRESENTATION_CONTEXT ( 3 ) GLOBAL_UNCERTAINTY_ASSIGNED_CONTEXT ( ( #2795 ) ) GLOBAL_UNIT_ASSIGNED_CONTEXT ( ( #28013, #1118, #21698 ) ) REPRESENTATION_CONTEXT ( 'NONE', 'WORKASPACE' ) );
#8628=CARTESIAN_POINT ( 'NONE',  ( 1.660531772554317831, -3.660093687634888848, -1.932505669160685592E-14 ) ) ;
#8646=AXIS2_PLACEMENT_3D ( 'NONE', #8675, #20272, #15392 ) ;
#8675=CARTESIAN_POINT ( 'NONE',  ( 0.000000000000000000, 0.000000000000000000, 0.000000000000000000 ) ) ;
#8777=CARTESIAN_POINT ( 'NONE',  ( 0.000000000000000000, 0.000000000000000000, -2.450000000000000622 ) ) ;
#8942=CARTESIAN_POINT ( 'NONE',  ( 0.000000000000000000, 0.000000000000000000, 19.04999999999997229 ) ) ;
#8976=VECTOR ( 'NONE', #4354, 1000.000000000000000 ) ;
#8996=EDGE_LOOP ( 'NONE', ( #14630, #9613, #29087 ) ) ;
#9007=CARTESIAN_POINT ( 'NONE',  ( 3.149999999999999023, 1.398881011027695624E-15, 1.700000000000000178 ) ) ;
#9008=VERTEX_POINT ( 'NONE', #15412 ) ;
#9037=CARTESIAN_POINT ( 'NONE',  ( 4.000000000000000000, -1.549102112939128917, -2.292104661404055665 ) ) ;
#9112=LINE ( 'NONE', #27793, #14617 ) ;
#9167=ADVANCED_FACE ( 'NONE', ( #29677 ), #28797, .T. ) ;
#9168=B_SPLINE_CURVE_WITH_KNOTS ( 'NONE', 3,
 ( #26531, #14744, #28692, #26383 ),
 .UNSPECIFIED., .F., .F.,
 ( 4, 4 ),
 ( 2.380737581781596564E-07, 0.002336974151641542981 ),
 .UNSPECIFIED. ) ;
#9173=DIRECTION ( 'NONE',  ( 0.000000000000000000, 0.000000000000000000, 1.000000000000000000 ) ) ;
#9184=CARTESIAN_POINT ( 'NONE',  ( -7.806255641895631925E-14, -4.618802153517044928, -2.092734410091829034 ) ) ;
#9187=ORIENTED_EDGE ( 'NONE', *, *, #10347, .F. ) ;
#9193=AXIS2_PLACEMENT_3D ( 'NONE', #13583, #22907, #20736 ) ;
#9204=EDGE_CURVE ( 'NONE', #4351, #2732, #502, .T. ) ;
#9206=CARTESIAN_POINT ( 'NONE',  ( 0.000000000000000000, 0.000000000000000000, 0.000000000000000000 ) ) ;
#9207=AXIS2_PLACEMENT_3D ( 'NONE', #24141, #10837, #15414 ) ;
#9230=AXIS2_PLACEMENT_3D ( 'NONE', #25114, #6350, #20662 ) ;
#9261=CIRCLE ( 'NONE', #5874, 4.000000000000000000 ) ;
#9337=VERTEX_POINT ( 'NONE', #4543 ) ;
#9339=DIRECTION ( 'NONE',  ( 0.000000000000000000, 0.000000000000000000, 1.000000000000000000 ) ) ;
#9357=CARTESIAN_POINT ( 'NONE',  ( -3.344563996438223885, -2.687817229851500844, -2.291324518471496319 ) ) ;
#9381=ORIENTED_EDGE ( 'NONE', *, *, #27325, .T. ) ;
#9398=ORIENTED_EDGE ( 'NONE', *, *, #18759, .T. ) ;
#9429=EDGE_CURVE ( 'NONE', #13842, #23922, #26535, .T. ) ;
#9485=ORIENTED_EDGE ( 'NONE', *, *, #12140, .F. ) ;
#9553=CARTESIAN_POINT ( 'NONE',  ( -4.000000000000003553, -6.938893903907228378E-15, -2.450000000000000178 ) ) ;
#9565=CARTESIAN_POINT ( 'NONE',  ( -2.500000000000002665, -1.110223024625156738E-15, -2.424599999999998978 ) ) ;
#9598=CARTESIAN_POINT ( 'NONE',  ( 0.000000000000000000, 0.000000000000000000, 0.000000000000000000 ) ) ;
#9599=COLOUR_RGB ( '', 0.72549020, 0.75294118, 0.79215686) ;
#9604=ORIENTED_EDGE ( 'NONE', *, *, #10025, .T. ) ;
#9613=ORIENTED_EDGE ( 'NONE', *, *, #22916, .F. ) ;
#9680=CARTESIAN_POINT ( 'NONE',  ( 2.000000000000026201, 3.464101615137736623, -2.450000000000000622 ) ) ;
#9703=CARTESIAN_POINT ( 'NONE',  ( -4.000000000000005329, 1.935983797701083420, -2.200530693383765168 ) ) ;
#9717=LINE ( 'NONE', #24084, #11975 ) ;
#9722=DIRECTION ( 'NONE',  ( 1.000000000000000000, 4.440892098500622217E-16, 0.000000000000000000 ) ) ;
#9739=CARTESIAN_POINT ( 'NONE',  ( 2.928571428571432378, 1.300546971703755312E-15, 2.549999999999998490 ) ) ;
#9740=FACE_OUTER_BOUND ( 'NONE', #14187, .T. ) ;
#9782=FACE_OUTER_BOUND ( 'NONE', #27241, .T. ) ;
#9855=AXIS2_PLACEMENT_3D ( 'NONE', #8942, #3940, #6831 ) ;
#9913=EDGE_LOOP ( 'NONE', ( #27759, #16274, #9187 ) ) ;
#9978=CARTESIAN_POINT ( 'NONE',  ( -0.6554360035617876612, 4.240386000424035906, -2.291324518471510974 ) ) ;
#10025=EDGE_CURVE ( 'NONE', #4487, #22117, #18803, .T. ) ;
#10082=CARTESIAN_POINT ( 'NONE',  ( -4.000000000000005329, 2.309401076758490934, -2.450000000000000178 ) ) ;
#10092=DIRECTION ( 'NONE',  ( 0.000000000000000000, 0.000000000000000000, 1.000000000000000000 ) ) ;
#10150=CONICAL_SURFACE ( 'NONE', #15509, 2.500000000000002665, 0.9599310885968781459 ) ;
#10152=ORIENTED_EDGE ( 'NONE', *, *, #12976, .F. ) ;
#10174=ADVANCED_FACE ( 'NONE', ( #22001 ), #10890, .T. ) ;
#10191=DIRECTION ( 'NONE',  ( -0.000000000000000000, -0.000000000000000000, 1.000000000000000000 ) ) ;
#10212=MECHANICAL_DESIGN_GEOMETRIC_PRESENTATION_REPRESENTATION('',(#20957),#3416);
#10229=AXIS2_PLACEMENT_3D ( 'NONE', #30176, #9339, #20791 ) ;
#10266=AXIS2_PLACEMENT_3D ( 'NONE', #10463, #19769, #19179 ) ;
#10312=B_SPLINE_CURVE_WITH_KNOTS ( 'NONE', 3,
 ( #6020, #15463, #1607, #3733, #18056, #6472 ),
 .UNSPECIFIED., .F., .F.,
 ( 4, 2, 4 ),
 ( 0.004120275011746852255, 0.005288420935197119671, 0.006456566858647387955 ),
 .UNSPECIFIED. ) ;
#10347=EDGE_CURVE ( 'NONE', #18869, #29035, #5442, .T. ) ;
#10416=FACE_OUTER_BOUND ( 'NONE', #22691, .T. ) ;
#10418=DIRECTION ( 'NONE',  ( -1.000000000000000000, -4.440892098500622217E-16, 0.000000000000000000 ) ) ;
#10446=DIRECTION ( 'NONE',  ( 1.000000000000000000, 0.000000000000000000, 0.000000000000000000 ) ) ;
#10463=CARTESIAN_POINT ( 'NONE',  ( 3.999999999999998224, 2.309401076758477167, -2.450000000000000178 ) ) ;
#10466=CARTESIAN_POINT ( 'NONE',  ( 0.000000000000000000, 0.000000000000000000, 9.480888224575629408 ) ) ;
#10516=ORIENTED_EDGE ( 'NONE', *, *, #5850, .T. ) ;
#10537=CARTESIAN_POINT ( 'NONE',  ( 0.000000000000000000, 0.000000000000000000, -2.450000000000000622 ) ) ;
#10563=FACE_OUTER_BOUND ( 'NONE', #24198, .T. ) ;
#10586=CARTESIAN_POINT ( 'NONE',  ( -2.000000000000032863, -3.464101615137743728, 8.673617379884035472E-16 ) ) ;
#10624=DIRECTION ( 'NONE',  ( 1.000000000000000000, 4.440892098500622217E-16, 0.000000000000000000 ) ) ;
#10627=FACE_OUTER_BOUND ( 'NONE', #28163, .T. ) ;
#10645=ORIENTED_EDGE ( 'NONE', *, *, #22203, .T. ) ;
#10665=CIRCLE ( 'NONE', #11166, 4.000000000000004441 ) ;
#10668=ORIENTED_EDGE ( 'NONE', *, *, #2111, .T. ) ;
#10752=CARTESIAN_POINT ( 'NONE',  ( -4.000000000000010658, -2.309401076758525573, -0.3572655899081716435 ) ) ;
#10837=DIRECTION ( 'NONE',  ( -0.5000000000000056621, -0.8660254037844354880, 0.000000000000000000 ) ) ;
#10853=ORIENTED_EDGE ( 'NONE', *, *, #11950, .F. ) ;
#10865=EDGE_CURVE ( 'NONE', #26865, #28553, #15852, .T. ) ;
#10882=DIRECTION ( 'NONE',  ( 0.000000000000000000, 0.000000000000000000, 1.000000000000000000 ) ) ;
#10890=CONICAL_SURFACE ( 'NONE', #13309, 4.000000000000003553, 1.047197551196597853 ) ;
#10911=CARTESIAN_POINT ( 'NONE',  ( 0.000000000000000000, 0.000000000000000000, 1.699999999999996625 ) ) ;
#10917=CARTESIAN_POINT ( 'NONE',  ( 2.000000000000003553, -3.464101615137736623, 8.673617379884035472E-16 ) ) ;
#10943=B_SPLINE_CURVE_WITH_KNOTS ( 'NONE', 3,
 ( #12861, #23189, #153, #25629 ),
 .UNSPECIFIED., .F., .F.,
 ( 4, 4 ),
 ( 2.380737581964190397E-07, 0.002336974151641511756 ),
 .UNSPECIFIED. ) ;
#10991=EDGE_CURVE ( 'NONE', #12786, #5044, #26712, .T. ) ;
#10999=ORIENTED_EDGE ( 'NONE', *, *, #22916, .T. ) ;
#11023=CONICAL_SURFACE ( 'NONE', #18830, 2.500000000000002665, 0.9599310885968781459 ) ;
#11032=ORIENTED_EDGE ( 'NONE', *, *, #22103, .T. ) ;
#11049=CIRCLE ( 'NONE', #12984, 0.8500000000000000888 ) ;
#11094=DIRECTION ( 'NONE',  ( -0.000000000000000000, -0.000000000000000000, 1.000000000000000000 ) ) ;
#11144=ORIENTED_EDGE ( 'NONE', *, *, #24594, .F. ) ;
#11166=AXIS2_PLACEMENT_3D ( 'NONE', #21641, #10191, #19960 ) ;
#11199=PRODUCT_DEFINITION_FORMATION_WITH_SPECIFIED_SOURCE ( 'ANY', '', #18122, .NOT_KNOWN. ) ;
#11213=FACE_OUTER_BOUND ( 'NONE', #6134, .T. ) ;
#11215=CYLINDRICAL_SURFACE ( 'NONE', #9230, 4.000000000000001776 ) ;
#11254=CARTESIAN_POINT ( 'NONE',  ( 2.000000000000026201, 3.464101615137736623, 8.673617379884035472E-16 ) ) ;
#11329=CARTESIAN_POINT ( 'NONE',  ( 2.000000000000003553, -3.464101615137736623, 8.673617379884035472E-16 ) ) ;
#11349=CARTESIAN_POINT ( 'NONE',  ( 3.999999999999980904, -2.309401076758567317, -0.3572655899081716435 ) ) ;
#11478=ORIENTED_EDGE ( 'NONE', *, *, #27970, .T. ) ;
#11536=ORIENTED_EDGE ( 'NONE', *, *, #23889, .T. ) ;
#11545=CARTESIAN_POINT ( 'NONE',  ( 4.000000000000003553, 2.309401076758525573, -0.3572655899081716435 ) ) ;
#11581=ORIENTED_EDGE ( 'NONE', *, *, #2182, .T. ) ;
#11590=EDGE_LOOP ( 'NONE', ( #29667, #28089, #11536, #10999, #24010, #116 ) ) ;
#11603=AXIS2_PLACEMENT_3D ( 'NONE', #19215, #19369, #2918 ) ;
#11605=CARTESIAN_POINT ( 'NONE',  ( 4.000000000000000000, 0.3904826640788077730, 4.917026258811211496E-16 ) ) ;
#11611=ORIENTED_EDGE ( 'NONE', *, *, #21000, .T. ) ;
#11639=CLOSED_SHELL ( 'NONE', ( #25218, #14053, #29257, #21600, #13443, #23039, #4910, #19517, #12682, #4813, #8110, #28452, #20239, #18982, #9167, #17821, #25490, #27932, #10174, #18521, #12410, #14776, #7708, #26671, #18336, #21424, #24444, #16583, #19775, #13037, #23458, #67, #1972 ) ) ;
#11657=DIRECTION ( 'NONE',  ( -0.000000000000000000, -0.000000000000000000, 1.000000000000000000 ) ) ;
#11686=MANIFOLD_SOLID_BREP ( 'TorqueElement', #11639 ) ;
#11692=EDGE_CURVE ( 'NONE', #14061, #17928, #29155, .T. ) ;
#11712=FACE_OUTER_BOUND ( 'NONE', #12981, .T. ) ;
#11933=ORIENTED_EDGE ( 'NONE', *, *, #11692, .T. ) ;
#11950=EDGE_CURVE ( 'NONE', #25602, #29938, #4447, .T. ) ;
#11969=FACE_BOUND ( 'NONE', #16123, .T. ) ;
#11974=CARTESIAN_POINT ( 'NONE',  ( -4.000000000000010658, -2.309401076758525573, -2.092734410091829034 ) ) ;
#11975=VECTOR ( 'NONE', #14446, 1000.000000000000000 ) ;
#11984=AXIS2_PLACEMENT_3D ( 'NONE', #27266, #22183, #1293 ) ;
#11996=CARTESIAN_POINT ( 'NONE',  ( -4.000000000000003553, 0.3904826640788011671, -2.449999999999998401 ) ) ;
#12070=CIRCLE ( 'NONE', #15490, 0.8500000000000000888 ) ;
#12113=DIRECTION ( 'NONE',  ( -1.000000000000000000, -4.440892098500622217E-16, 0.000000000000000000 ) ) ;
#12115=CARTESIAN_POINT ( 'NONE',  ( 3.150000000000000799, 1.398881011027696413E-15, 2.550000000000000266 ) ) ;
#12140=EDGE_CURVE ( 'NONE', #26865, #4487, #17272, .T. ) ;
#12251=VERTEX_POINT ( 'NONE', #14932 ) ;
#12274=CARTESIAN_POINT ( 'NONE',  ( -1.660531772554310725, 3.660093687634845772, 4.223306275009939913E-15 ) ) ;
#12278=CARTESIAN_POINT ( 'NONE',  ( 3.344563996438202569, 2.687817229851458212, -2.291324518471520300 ) ) ;
#12378=DIRECTION ( 'NONE',  ( 1.000000000000000000, 4.440892098500622217E-16, 0.000000000000000000 ) ) ;
#12410=ADVANCED_FACE ( 'NONE', ( #24879 ), #20339, .T. ) ;
#12440=ORIENTED_EDGE ( 'NONE', *, *, #25211, .F. ) ;
#12450=VECTOR ( 'NONE', #19779, 1000.000000000000000 ) ;
#12516=CARTESIAN_POINT ( 'NONE',  ( 2.500000000000002665, 1.416384724411995397E-15, -2.424599999999998978 ) ) ;
#12546=CARTESIAN_POINT ( 'NONE',  ( 3.999999999999980904, -2.309401076758567317, -0.3572655899081716435 ) ) ;
#12552=EDGE_CURVE ( 'NONE', #6921, #15438, #19619, .T. ) ;
#12579=CARTESIAN_POINT ( 'NONE',  ( 0.000000000000000000, 0.000000000000000000, 0.000000000000000000 ) ) ;
#12611=CYLINDRICAL_SURFACE ( 'NONE', #26681, 2.100000000000000977 ) ;
#12682=ADVANCED_FACE ( 'NONE', ( #5902 ), #15183, .T. ) ;
#12721=DIRECTION ( 'NONE',  ( 0.000000000000000000, 0.000000000000000000, -1.000000000000000000 ) ) ;
#12786=VERTEX_POINT ( 'NONE', #22980 ) ;
#12799=EDGE_CURVE ( 'NONE', #8506, #29328, #2856, .T. ) ;
#12804=ORIENTED_EDGE ( 'NONE', *, *, #9204, .F. ) ;
#12861=CARTESIAN_POINT ( 'NONE',  ( 3.999999999999980904, -2.309401076758567317, -2.092734410091829034 ) ) ;
#12870=CYLINDRICAL_SURFACE ( 'NONE', #11984, 2.500000000000002665 ) ;
#12976=EDGE_CURVE ( 'NONE', #9008, #14061, #7947, .T. ) ;
#12981=EDGE_LOOP ( 'NONE', ( #12804, #23606, #15886, #22099, #16872, #21071 ) ) ;
#12982=ORIENTED_EDGE ( 'NONE', *, *, #19136, .T. ) ;
#12984=AXIS2_PLACEMENT_3D ( 'NONE', #3560, #22324, #15282 ) ;
#13017=FACE_OUTER_BOUND ( 'NONE', #13755, .T. ) ;
#13037=ADVANCED_FACE ( 'NONE', ( #9782 ), #3243, .F. ) ;
#13054=CARTESIAN_POINT ( 'NONE',  ( 1.214306433183764966E-14, 4.618802153517016507, -2.450000000000000178 ) ) ;
#13074=AXIS2_PLACEMENT_3D ( 'NONE', #19097, #16661, #14800 ) ;
#13190=AXIS2_PLACEMENT_3D ( 'NONE', #5435, #19606, #10446 ) ;
#13228=ORIENTED_EDGE ( 'NONE', *, *, #24395, .F. ) ;
#13309=AXIS2_PLACEMENT_3D ( 'NONE', #10537, #28603, #12378 ) ;
#13313=DIRECTION ( 'NONE',  ( 0.000000000000000000, 0.000000000000000000, 1.000000000000000000 ) ) ;
#13331=CARTESIAN_POINT ( 'NONE',  ( 4.000000000000000000, -0.7779732554280925916, -2.416455648918321764 ) ) ;
#13412=EDGE_CURVE ( 'NONE', #26117, #29919, #25759, .T. ) ;
#13443=ADVANCED_FACE ( 'NONE', ( #28573 ), #10150, .F. ) ;
#13449=DIRECTION ( 'NONE',  ( 4.440892098500622217E-16, -1.000000000000000000, 0.000000000000000000 ) ) ;
#13513=CARTESIAN_POINT ( 'NONE',  ( 4.000000000000003553, 2.309401076758525573, -2.092734410091829034 ) ) ;
#13526=EDGE_CURVE ( 'NONE', #8103, #7935, #5948, .T. ) ;
#13572=DIRECTION ( 'NONE',  ( -1.000000000000000000, -4.440892098500622217E-16, 0.000000000000000000 ) ) ;
#13577=CARTESIAN_POINT ( 'NONE',  ( 2.000000000000026201, 3.464101615137736623, 8.673617379884035472E-16 ) ) ;
#13583=CARTESIAN_POINT ( 'NONE',  ( 0.000000000000000000, 0.000000000000000000, 1.700000000000000178 ) ) ;
#13598=CARTESIAN_POINT ( 'NONE',  ( 0.000000000000000000, 0.000000000000000000, -2.424599999999998978 ) ) ;
#13628=CARTESIAN_POINT ( 'NONE',  ( -4.000000000000001776, 2.309401076758532678, -2.092734410091829034 ) ) ;
#13644=CONICAL_SURFACE ( 'NONE', #26349, 4.000000000000003553, 1.047197551196597853 ) ;
#13729=CARTESIAN_POINT ( 'NONE',  ( 4.000000000000000000, 0.000000000000000000, -2.450000000000000622 ) ) ;
#13751=PRODUCT_CONTEXT ( 'NONE', #28636, 'mechanical' ) ;
#13755=EDGE_LOOP ( 'NONE', ( #12982, #2916, #26807 ) ) ;
#13762=UNCERTAINTY_MEASURE_WITH_UNIT (LENGTH_MEASURE( 1.000000000000000082E-05 ), #1729, 'distance_accuracy_value', 'NONE');
#13831=CARTESIAN_POINT ( 'NONE',  ( 2.500000000000002665, 1.110223024625156738E-15, 19.04999999999997229 ) ) ;
#13832=CIRCLE ( 'NONE', #703, 4.000000000000004441 ) ;
#13838=CARTESIAN_POINT ( 'NONE',  ( 2.339468227445709925, 3.268109542640640353, 5.126666913256651224E-15 ) ) ;
#13842=VERTEX_POINT ( 'NONE', #18588 ) ;
#13866=CARTESIAN_POINT ( 'NONE',  ( -4.000000000000005329, 2.309401076758490934, -0.3572655899081616515 ) ) ;
#13916=CARTESIAN_POINT ( 'NONE',  ( -2.000000000000026201, -3.464101615137764156, -2.450000000000000622 ) ) ;
#13925=EDGE_CURVE ( 'NONE', #6899, #9337, #9717, .T. ) ;
#13941=LINE ( 'NONE', #7252, #8976 ) ;
#13982=B_SPLINE_CURVE_WITH_KNOTS ( 'NONE', 3,
 ( #17161, #21592, #691, #9978, #19294, #28651 ),
 .UNSPECIFIED., .F., .F.,
 ( 4, 2, 4 ),
 ( 0.002336974151641542981, 0.003500975885716449756, 0.004664977619791356098 ),
 .UNSPECIFIED. ) ;
#13994=ORIENTED_EDGE ( 'NONE', *, *, #13925, .F. ) ;
#14053=ADVANCED_FACE ( 'NONE', ( #28245 ), #29094, .T. ) ;
#14061=VERTEX_POINT ( 'NONE', #9565 ) ;
#14080=CARTESIAN_POINT ( 'NONE',  ( 3.999999999999996447, 0.000000000000000000, 8.673617379884035472E-16 ) ) ;
#14187=EDGE_LOOP ( 'NONE', ( #29079, #4627, #8572 ) ) ;
#14210=DIRECTION ( 'NONE',  ( 0.000000000000000000, 0.000000000000000000, 1.000000000000000000 ) ) ;
#14219=CARTESIAN_POINT ( 'NONE',  ( -1.318516776095816523, -3.857556137907101501, -2.449999999999979305 ) ) ;
#14236=EDGE_CURVE ( 'NONE', #4351, #8506, #17645, .T. ) ;
#14241=CARTESIAN_POINT ( 'NONE',  ( -2.000000000000026201, -3.464101615137764156, -2.450000000000000622 ) ) ;
#14279=DIRECTION ( 'NONE',  ( 0.000000000000000000, 0.000000000000000000, -1.000000000000000000 ) ) ;
#14292=EDGE_LOOP ( 'NONE', ( #9381, #4379 ) ) ;
#14345=EDGE_LOOP ( 'NONE', ( #7192, #736, #4433, #17424 ) ) ;
#14408=DIRECTION ( 'NONE',  ( 0.000000000000000000, 0.000000000000000000, -1.000000000000000000 ) ) ;
#14446=DIRECTION ( 'NONE',  ( 0.000000000000000000, 0.000000000000000000, 1.000000000000000000 ) ) ;
#14447=ORIENTED_EDGE ( 'NONE', *, *, #18518, .F. ) ;
#14517=AXIS2_PLACEMENT_3D ( 'NONE', #10911, #1933, #20368 ) ;
#14560=FACE_OUTER_BOUND ( 'NONE', #397, .T. ) ;
#14601=CARTESIAN_POINT ( 'NONE',  ( 0.000000000000000000, 0.000000000000000000, 0.000000000000000000 ) ) ;
#14617=VECTOR ( 'NONE', #6857, 1000.000000000000000 ) ;
#14624=DIRECTION ( 'NONE',  ( -0.000000000000000000, -0.000000000000000000, 1.000000000000000000 ) ) ;
#14630=ORIENTED_EDGE ( 'NONE', *, *, #10991, .T. ) ;
#14643=FACE_OUTER_BOUND ( 'NONE', #9913, .T. ) ;
#14676=ORIENTED_EDGE ( 'NONE', *, *, #18518, .T. ) ;
#14727=ORIENTED_EDGE ( 'NONE', *, *, #16415, .F. ) ;
#14744=CARTESIAN_POINT ( 'NONE',  ( -3.345653888883662663, 2.687187980154698064, -2.310849780464865333 ) ) ;
#14746=CARTESIAN_POINT ( 'NONE',  ( -4.000000000000003553, -6.938893903907228378E-15, 8.673617379884035472E-16 ) ) ;
#14776=ADVANCED_FACE ( 'NONE', ( #19746 ), #23720, .T. ) ;
#14800=DIRECTION ( 'NONE',  ( 1.000000000000000000, 4.440892098500622217E-16, 0.000000000000000000 ) ) ;
#14819=B_SPLINE_CURVE_WITH_KNOTS ( 'NONE', 3,
 ( #2479, #2328, #7485, #25650, #18478, #474 ),
 .UNSPECIFIED., .F., .F.,
 ( 4, 2, 4 ),
 ( 0.002336974151641603697, 0.003500975885716479247, 0.004664977619791355230 ),
 .UNSPECIFIED. ) ;
#14882=CARTESIAN_POINT ( 'NONE',  ( -2.000000000000008882, 3.464101615137750390, -2.450000000000000622 ) ) ;
#14926=ORIENTED_EDGE ( 'NONE', *, *, #9429, .T. ) ;
#14932=CARTESIAN_POINT ( 'NONE',  ( -3.149999999999998135, -1.149807694518792937E-15, 2.550000000000000266 ) ) ;
#14942=ORIENTED_EDGE ( 'NONE', *, *, #15410, .F. ) ;
#14990=EDGE_CURVE ( 'NONE', #15438, #5490, #7465, .T. ) ;
#15002=CARTESIAN_POINT ( 'NONE',  ( 0.000000000000000000, 0.000000000000000000, 0.000000000000000000 ) ) ;
#15140=DIRECTION ( 'NONE',  ( 0.5000000000000029976, -0.8660254037844370423, 0.000000000000000000 ) ) ;
#15183=PLANE ( 'NONE',  #29675 ) ;
#15258=DIRECTION ( 'NONE',  ( 1.000000000000000000, 4.440892098500622217E-16, 0.000000000000000000 ) ) ;
#15271=DIRECTION ( 'NONE',  ( 1.000000000000000000, 4.440892098500622217E-16, 0.000000000000000000 ) ) ;
#15272=DIRECTION ( 'NONE',  ( -0.000000000000000000, -0.000000000000000000, 1.000000000000000000 ) ) ;
#15282=DIRECTION ( 'NONE',  ( -1.000000000000000000, -3.216245299353269257E-16, 0.000000000000000000 ) ) ;
#15283=SURFACE_STYLE_USAGE ( .BOTH. , #20624 ) ;
#15321=B_SPLINE_CURVE_WITH_KNOTS ( 'NONE', 3,
 ( #20360, #18683, #15935, #9357, #4201, #22975 ),
 .UNSPECIFIED., .F., .F.,
 ( 4, 2, 4 ),
 ( 0.002336974151641586783, 0.003500975885716471007, 0.004664977619791355230 ),
 .UNSPECIFIED. ) ;
#15341=DIRECTION ( 'NONE',  ( 0.000000000000000000, 0.000000000000000000, 1.000000000000000000 ) ) ;
#15392=DIRECTION ( 'NONE',  ( -1.000000000000000000, -4.440892098500622217E-16, 0.000000000000000000 ) ) ;
#15410=EDGE_CURVE ( 'NONE', #8506, #12251, #11049, .T. ) ;
#15412=CARTESIAN_POINT ( 'NONE',  ( -2.099999999999999645, -6.754115128641864009E-16, -2.144516984716112518 ) ) ;
#15414=DIRECTION ( 'NONE',  ( 0.8660254037844353769, -0.5000000000000055511, 0.000000000000000000 ) ) ;
#15431=DIRECTION ( 'NONE',  ( -1.000000000000000000, -4.440892098500622217E-16, 0.000000000000000000 ) ) ;
#15438=VERTEX_POINT ( 'NONE', #12546 ) ;
#15445=MECHANICAL_DESIGN_GEOMETRIC_PRESENTATION_REPRESENTATION('',(#24242),#8622);
#15463=CARTESIAN_POINT ( 'NONE',  ( -4.000000000000003553, -1.933795701539605227, -2.201162342337703137 ) ) ;
#15490=AXIS2_PLACEMENT_3D ( 'NONE', #9007, #13449, #2180 ) ;
#15509=AXIS2_PLACEMENT_3D ( 'NONE', #21515, #21657, #21816 ) ;
#15590=CARTESIAN_POINT ( 'NONE',  ( -2.100000000000000977, -6.754115128641868940E-16, 1.700000000000000178 ) ) ;
#15594=CARTESIAN_POINT ( 'NONE',  ( 4.000000000000003553, 2.309401076758525573, -0.3572655899081716435 ) ) ;
#15652=B_SPLINE_CURVE_WITH_KNOTS ( 'NONE', 3,
 ( #26905, #17108, #26437, #13577 ),
 .UNSPECIFIED., .F., .F.,
 ( 4, 4 ),
 ( 2.380737581676867028E-07, 0.002336974151641585049 ),
 .UNSPECIFIED. ) ;
#15655=DIRECTION ( 'NONE',  ( 1.000000000000000000, 4.440892098500622217E-16, 0.000000000000000000 ) ) ;
#15672=CYLINDRICAL_SURFACE ( 'NONE', #9855, 2.500000000000002665 ) ;
#15676=ORIENTED_EDGE ( 'NONE', *, *, #17176, .T. ) ;
#15718=ORIENTED_EDGE ( 'NONE', *, *, #26, .T. ) ;
#15733=ORIENTED_EDGE ( 'NONE', *, *, #12140, .T. ) ;
#15741=PRESENTATION_STYLE_ASSIGNMENT (( #15283 ) ) ;
#15748=EDGE_CURVE ( 'NONE', #5490, #29035, #16544, .T. ) ;
#15782=ORIENTED_EDGE ( 'NONE', *, *, #7320, .T. ) ;
#15821=DIRECTION ( 'NONE',  ( 1.000000000000000000, 4.440892098500622217E-16, 0.000000000000000000 ) ) ;
#15852=CIRCLE ( 'NONE', #2709, 4.000000000000004441 ) ;
#15864=ORIENTED_EDGE ( 'NONE', *, *, #5895, .F. ) ;
#15872=AXIS2_PLACEMENT_3D ( 'NONE', #5458, #26530, #16895 ) ;
#15877=DIRECTION ( 'NONE',  ( 0.000000000000000000, 0.000000000000000000, 1.000000000000000000 ) ) ;
#15883=VECTOR ( 'NONE', #26583, 1000.000000000000114 ) ;
#15886=ORIENTED_EDGE ( 'NONE', *, *, #5714, .F. ) ;
#15935=CARTESIAN_POINT ( 'NONE',  ( -2.678494666091066456, -3.072372537026392791, -2.415789719053448970 ) ) ;
#15940=DIRECTION ( 'NONE',  ( -0.8660254037844370423, -0.5000000000000027756, 0.000000000000000000 ) ) ;
#15948=DIRECTION ( 'NONE',  ( 0.000000000000000000, 0.000000000000000000, 1.000000000000000000 ) ) ;
#15978=FACE_BOUND ( 'NONE', #14292, .T. ) ;
#15986=CARTESIAN_POINT ( 'NONE',  ( 2.678494666091048693, 3.072372537026350159, -0.03421028094652719953 ) ) ;
#16076=CARTESIAN_POINT ( 'NONE',  ( 4.000000000000000000, -0.7779732554280925916, -0.03354435108167886509 ) ) ;
#16084=DIRECTION ( 'NONE',  ( -1.000000000000000000, -4.440892098500622217E-16, 0.000000000000000000 ) ) ;
#16123=EDGE_LOOP ( 'NONE', ( #29541, #27238 ) ) ;
#16129=FACE_OUTER_BOUND ( 'NONE', #6667, .T. ) ;
#16139=CARTESIAN_POINT ( 'NONE',  ( 3.673643420401897952, 2.497823135841248821, -0.2484800633749905674 ) ) ;
#16160=B_SPLINE_CURVE_WITH_KNOTS ( 'NONE', 3,
 ( #19443, #12274, #28814, #7852, #17303, #26642 ),
 .UNSPECIFIED., .F., .F.,
 ( 4, 2, 4 ),
 ( 0.002336974151641542981, 0.003500975885716449756, 0.004664977619791356098 ),
 .UNSPECIFIED. ) ;
#16161=ORIENTED_EDGE ( 'NONE', *, *, #26108, .T. ) ;
#16167=CARTESIAN_POINT ( 'NONE',  ( 0.000000000000000000, 0.000000000000000000, 1.700000000000000178 ) ) ;
#16169=DIRECTION ( 'NONE',  ( -0.000000000000000000, -0.000000000000000000, 1.000000000000000000 ) ) ;
#16228=ORIENTED_EDGE ( 'NONE', *, *, #3077, .T. ) ;
#16255=ORIENTED_EDGE ( 'NONE', *, *, #3600, .T. ) ;
#16274=ORIENTED_EDGE ( 'NONE', *, *, #15748, .T. ) ;
#16415=EDGE_CURVE ( 'NONE', #17928, #14061, #5992, .T. ) ;
#16419=EDGE_LOOP ( 'NONE', ( #14676, #11478 ) ) ;
#16429=AXIS2_PLACEMENT_3D ( 'NONE', #18594, #23630, #25325 ) ;
#16446=VECTOR ( 'NONE', #24670, 1000.000000000000000 ) ;
#16544=B_SPLINE_CURVE_WITH_KNOTS ( 'NONE', 3,
 ( #2335, #11605, #20919, #18645, #27991, #15594 ),
 .UNSPECIFIED., .F., .F.,
 ( 4, 2, 4 ),
 ( 0.006456566858647419180, 0.007625406818786685526, 0.008794246778925951871 ),
 .UNSPECIFIED. ) ;
#16552=PLANE ( 'NONE',  #28030 ) ;
#16583=ADVANCED_FACE ( 'NONE', ( #22709 ), #15672, .F. ) ;
#16661=DIRECTION ( 'NONE',  ( 0.000000000000000000, 0.000000000000000000, 1.000000000000000000 ) ) ;
#16676=FILL_AREA_STYLE_COLOUR ( '', #9599 ) ;
#16707=DIRECTION ( 'NONE',  ( 0.000000000000000000, 0.000000000000000000, -1.000000000000000000 ) ) ;
#16717=CARTESIAN_POINT ( 'NONE',  ( 2.339468227445709925, 3.268109542640638576, -2.450000000000006395 ) ) ;
#16742=CARTESIAN_POINT ( 'NONE',  ( -4.000000000000001776, 2.309401076758532678, -2.092734410091829034 ) ) ;
#16757=ORIENTED_EDGE ( 'NONE', *, *, #9429, .F. ) ;
#16872=ORIENTED_EDGE ( 'NONE', *, *, #27045, .T. ) ;
#16877=AXIS2_PLACEMENT_3D ( 'NONE', #15002, #12721, #17159 ) ;
#16889=CYLINDRICAL_SURFACE ( 'NONE', #23450, 2.100000000000000977 ) ;
#16895=DIRECTION ( 'NONE',  ( 1.000000000000000000, 4.440892098500622217E-16, 0.000000000000000000 ) ) ;
#16992=ORIENTED_EDGE ( 'NONE', *, *, #22203, .F. ) ;
#17042=CARTESIAN_POINT ( 'NONE',  ( -4.000000000000003553, 1.557668341133518153, -2.290303434304242547 ) ) ;
#17047=DIRECTION ( 'NONE',  ( 1.000000000000000000, 4.440892098500623203E-16, 0.000000000000000000 ) ) ;
#17108=CARTESIAN_POINT ( 'NONE',  ( 0.6543461111163458854, 4.241015250120808489, -0.1391502195351409232 ) ) ;
#17115=FACE_OUTER_BOUND ( 'NONE', #25970, .T. ) ;
#17121=VECTOR ( 'NONE', #28662, 1000.000000000000000 ) ;
#17136=ORIENTED_EDGE ( 'NONE', *, *, #21098, .F. ) ;
#17147=DIRECTION ( 'NONE',  ( 0.000000000000000000, 0.000000000000000000, -1.000000000000000000 ) ) ;
#17153=FACE_OUTER_BOUND ( 'NONE', #16419, .T. ) ;
#17159=DIRECTION ( 'NONE',  ( -1.000000000000000000, -4.440892098500622217E-16, 0.000000000000000000 ) ) ;
#17161=CARTESIAN_POINT ( 'NONE',  ( -2.000000000000008882, 3.464101615137750390, -2.450000000000000622 ) ) ;
#17176=EDGE_CURVE ( 'NONE', #29938, #7935, #18665, .T. ) ;
#17272=B_SPLINE_CURVE_WITH_KNOTS ( 'NONE', 3,
 ( #2621, #7189, #19079, #25808, #4890, #2325 ),
 .UNSPECIFIED., .F., .F.,
 ( 4, 2, 4 ),
 ( 0.002336974151641511756, 0.003500975885716454961, 0.004664977619791398598 ),
 .UNSPECIFIED. ) ;
#17296=PLANE ( 'NONE',  #5597 ) ;
#17303=CARTESIAN_POINT ( 'NONE',  ( -0.3263565795980836737, 4.430380094434250182, -0.2484800633750045007 ) ) ;
#17340=DIRECTION ( 'NONE',  ( 1.000000000000000000, 4.440892098500623203E-16, 0.000000000000000000 ) ) ;
#17398=DIRECTION ( 'NONE',  ( 0.000000000000000000, 0.000000000000000000, 1.000000000000000000 ) ) ;
#17424=ORIENTED_EDGE ( 'NONE', *, *, #16415, .T. ) ;
#17501=EDGE_LOOP ( 'NONE', ( #6998, #22154, #26386, #4377, #3714, #1432 ) ) ;
#17562=EDGE_LOOP ( 'NONE', ( #9604, #16255, #25770, #13994, #20747, #20454 ) ) ;
#17570=ORIENTED_EDGE ( 'NONE', *, *, #1168, .F. ) ;
#17645=LINE ( 'NONE', #6215, #12450 ) ;
#17733=AXIS2_PLACEMENT_3D ( 'NONE', #16167, #13313, #25940 ) ;
#17755=ORIENTED_EDGE ( 'NONE', *, *, #13412, .F. ) ;
#17821=ADVANCED_FACE ( 'NONE', ( #11213 ), #8437, .T. ) ;
#17867=CARTESIAN_POINT ( 'NONE',  ( -4.000000000000003553, 1.557668341133489953, -0.1596965656957523294 ) ) ;
#17886=FACE_OUTER_BOUND ( 'NONE', #5465, .T. ) ;
#17928=VERTEX_POINT ( 'NONE', #25410 ) ;
#17964=CARTESIAN_POINT ( 'NONE',  ( 0.000000000000000000, 0.000000000000000000, -2.450000000000000178 ) ) ;
#18056=CARTESIAN_POINT ( 'NONE',  ( -4.000000000000004441, -0.3902508023145587202, -2.449999999999998401 ) ) ;
#18089=CARTESIAN_POINT ( 'NONE',  ( 0.3263565795980569728, -4.430380094434312355, -0.2484800633750388621 ) ) ;
#18091=CARTESIAN_POINT ( 'NONE',  ( 0.000000000000000000, 0.000000000000000000, 2.549999999999998490 ) ) ;
#18112=VERTEX_POINT ( 'NONE', #14241 ) ;
#18122=PRODUCT ( 'torque nut 08_iso_ISO 10511-M5-N', 'torque nut 08_iso_ISO 10511-M5-N', '', ( #13751 ) ) ;
#18171=CARTESIAN_POINT ( 'NONE',  ( 2.928571428571432378, 1.300546971703755312E-15, 9.480888224575629408 ) ) ;
#18290=DIRECTION ( 'NONE',  ( 0.000000000000000000, 0.000000000000000000, -1.000000000000000000 ) ) ;
#18336=ADVANCED_FACE ( 'NONE', ( #13017 ), #1651, .T. ) ;
#18338=EDGE_CURVE ( 'NONE', #6921, #26865, #10943, .T. ) ;
#18347=UNCERTAINTY_MEASURE_WITH_UNIT (LENGTH_MEASURE( 1.000000000000000082E-05 ), #28940, 'distance_accuracy_value', 'NONE');
#18478=CARTESIAN_POINT ( 'NONE',  ( -3.673643420401923265, -2.497823135841289677, -0.2484800633750157139 ) ) ;
#18518=EDGE_CURVE ( 'NONE', #25602, #8103, #23115, .T. ) ;
#18521=ADVANCED_FACE ( 'NONE', ( #9740 ), #3617, .T. ) ;
#18538=CARTESIAN_POINT ( 'NONE',  ( 1.214306433183764966E-14, 4.618802153517016507, -2.450000000000000178 ) ) ;
#18588=CARTESIAN_POINT ( 'NONE',  ( -4.000000000000003553, -6.938893903907228378E-15, -2.450000000000000178 ) ) ;
#18594=CARTESIAN_POINT ( 'NONE',  ( 0.000000000000000000, 0.000000000000000000, 9.480888224575629408 ) ) ;
#18613=CARTESIAN_POINT ( 'NONE',  ( 0.000000000000000000, 0.000000000000000000, 0.000000000000000000 ) ) ;
#18645=CARTESIAN_POINT ( 'NONE',  ( 4.000000000000000000, 1.557668341133518819, -0.1596965656957546609 ) ) ;
#18649=AXIS2_PLACEMENT_3D ( 'NONE', #27019, #5776, #29323 ) ;
#18660=DIRECTION ( 'NONE',  ( 0.000000000000000000, 0.000000000000000000, 1.000000000000000000 ) ) ;
#18665=CIRCLE ( 'NONE', #21585, 2.928571428571432378 ) ;
#18683=CARTESIAN_POINT ( 'NONE',  ( -2.339468227445728132, -3.268109542640681209, -2.449999999999980194 ) ) ;
#18726=PLANE ( 'NONE',  #7037 ) ;
#18759=EDGE_CURVE ( 'NONE', #12786, #4780, #13832, .T. ) ;
#18803=LINE ( 'NONE', #19106, #20184 ) ;
#18811=CARTESIAN_POINT ( 'NONE',  ( -0.6543461111163901833, -4.241015250120830693, -2.310849780464841352 ) ) ;
#18830=AXIS2_PLACEMENT_3D ( 'NONE', #13598, #27235, #15431 ) ;
#18846=CARTESIAN_POINT ( 'NONE',  ( 2.678494666091048693, 3.072372537026350159, -2.415789719053474283 ) ) ;
#18857=EDGE_LOOP ( 'NONE', ( #20273, #5550, #30242, #15864 ) ) ;
#18869=VERTEX_POINT ( 'NONE', #11254 ) ;
#18949=ORIENTED_EDGE ( 'NONE', *, *, #20270, .T. ) ;
#18982=ADVANCED_FACE ( 'NONE', ( #15978, #16129 ), #18726, .T. ) ;
#19029=EDGE_CURVE ( 'NONE', #23789, #17928, #4542, .T. ) ;
#19079=CARTESIAN_POINT ( 'NONE',  ( 1.321505333908960633, -3.855830693249187480, -2.415789719053445417 ) ) ;
#19097=CARTESIAN_POINT ( 'NONE',  ( 0.000000000000000000, 0.000000000000000000, 9.480888224575629408 ) ) ;
#19106=CARTESIAN_POINT ( 'NONE',  ( -3.469446951953614189E-15, -4.618802153517058251, -2.450000000000000178 ) ) ;
#19136=EDGE_CURVE ( 'NONE', #2732, #18869, #30008, .T. ) ;
#19172=DIRECTION ( 'NONE',  ( -1.000000000000000000, -4.440892098500622217E-16, 0.000000000000000000 ) ) ;
#19179=DIRECTION ( 'NONE',  ( 0.000000000000000000, 0.000000000000000000, 1.000000000000000000 ) ) ;
#19207=ORIENTED_EDGE ( 'NONE', *, *, #18759, .F. ) ;
#19215=CARTESIAN_POINT ( 'NONE',  ( 0.000000000000000000, 0.000000000000000000, 1.700000000000000178 ) ) ;
#19286=AXIS2_PLACEMENT_3D ( 'NONE', #9598, #5339, #2756 ) ;
#19294=CARTESIAN_POINT ( 'NONE',  ( -0.3263565795980836182, 4.430380094434250182, -2.201519936624996010 ) ) ;
#19319=CARTESIAN_POINT ( 'NONE',  ( 0.000000000000000000, 0.000000000000000000, 0.000000000000000000 ) ) ;
#19336=VERTEX_POINT ( 'NONE', #19926 ) ;
#19365=EDGE_CURVE ( 'NONE', #461, #4135, #25116, .T. ) ;
#19369=DIRECTION ( 'NONE',  ( 0.000000000000000000, 0.000000000000000000, 1.000000000000000000 ) ) ;
#19430=AXIS2_PLACEMENT_3D ( 'NONE', #22560, #11094, #3938 ) ;
#19432=DIRECTION ( 'NONE',  ( -1.000000000000000000, -4.440892098500622217E-16, -0.000000000000000000 ) ) ;
#19443=CARTESIAN_POINT ( 'NONE',  ( -2.000000000000008882, 3.464101615137750390, 0.000000000000000000 ) ) ;
#19469=EDGE_LOOP ( 'NONE', ( #15733, #10516, #10668 ) ) ;
#19470=DIRECTION ( 'NONE',  ( -0.8660254037844348218, 0.5000000000000065503, -0.000000000000000000 ) ) ;
#19517=ADVANCED_FACE ( 'NONE', ( #30050 ), #16552, .T. ) ;
#19542=EDGE_CURVE ( 'NONE', #5490, #29328, #13941, .T. ) ;
#19582=FACE_OUTER_BOUND ( 'NONE', #21854, .T. ) ;
#19606=DIRECTION ( 'NONE',  ( 0.000000000000000000, 0.000000000000000000, 1.000000000000000000 ) ) ;
#19619=LINE ( 'NONE', #3461, #16446 ) ;
#19695=VECTOR ( 'NONE', #23611, 1000.000000000000000 ) ;
#19724=CARTESIAN_POINT ( 'NONE',  ( -3.469446951953614189E-15, -4.618802153517058251, -2.450000000000000178 ) ) ;
#19740=CARTESIAN_POINT ( 'NONE',  ( 3.999999999999996447, 0.000000000000000000, 8.673617379884035472E-16 ) ) ;
#19746=FACE_OUTER_BOUND ( 'NONE', #20472, .T. ) ;
#19769=DIRECTION ( 'NONE',  ( -1.000000000000000000, -4.440892098500622217E-16, 0.000000000000000000 ) ) ;
#19773=DIRECTION ( 'NONE',  ( 0.000000000000000000, 0.000000000000000000, 1.000000000000000000 ) ) ;
#19775=ADVANCED_FACE ( 'NONE', ( #682, #17153 ), #17296, .F. ) ;
#19779=DIRECTION ( 'NONE',  ( 0.000000000000000000, 0.000000000000000000, 1.000000000000000000 ) ) ;
#19802=APPLICATION_CONTEXT ( 'automotive_design' ) ;
#19859=CARTESIAN_POINT ( 'NONE',  ( 0.000000000000000000, 0.000000000000000000, -2.450000000000000622 ) ) ;
#19913=ORIENTED_EDGE ( 'NONE', *, *, #5848, .T. ) ;
#19926=CARTESIAN_POINT ( 'NONE',  ( -4.000000000000005329, 2.309401076758490934, -0.3572655899081616515 ) ) ;
#19957=CARTESIAN_POINT ( 'NONE',  ( 0.000000000000000000, 0.000000000000000000, 2.549999999999998490 ) ) ;
#19960=DIRECTION ( 'NONE',  ( -1.000000000000000000, -1.332267629550187651E-15, 0.000000000000000000 ) ) ;
#19964=DIRECTION ( 'NONE',  ( -1.000000000000000000, -1.332267629550187651E-15, 0.000000000000000000 ) ) ;
#19981=ORIENTED_EDGE ( 'NONE', *, *, #19542, .T. ) ;
#19988=CIRCLE ( 'NONE', #7809, 4.000000000000003553 ) ;
#20030=EDGE_LOOP ( 'NONE', ( #28441, #1680, #4766, #26596 ) ) ;
#20050=CARTESIAN_POINT ( 'NONE',  ( -7.806255641895631925E-14, -4.618802153517044928, -0.3572655899081716435 ) ) ;
#20141=CARTESIAN_POINT ( 'NONE',  ( -4.000000000000000000, -1.286498119741307703E-15, 1.699999999999996625 ) ) ;
#20178=VECTOR ( 'NONE', #27135, 1000.000000000000000 ) ;
#20184=VECTOR ( 'NONE', #18660, 1000.000000000000000 ) ;
#20221=CIRCLE ( 'NONE', #25600, 4.000000000000003553 ) ;
#20239=ADVANCED_FACE ( 'NONE', ( #17115 ), #26289, .T. ) ;
#20256=DIRECTION ( 'NONE',  ( -0.000000000000000000, -0.000000000000000000, 1.000000000000000000 ) ) ;
#20270=EDGE_CURVE ( 'NONE', #3702, #4351, #20221, .T. ) ;
#20272=DIRECTION ( 'NONE',  ( 0.000000000000000000, 0.000000000000000000, -1.000000000000000000 ) ) ;
#20273=ORIENTED_EDGE ( 'NONE', *, *, #3077, .F. ) ;
#20302=CIRCLE ( 'NONE', #5204, 4.000000000000004441 ) ;
#20339=CONICAL_SURFACE ( 'NONE', #8646, 4.000000000000003553, 1.047197551196597853 ) ;
#20360=CARTESIAN_POINT ( 'NONE',  ( -2.000000000000026201, -3.464101615137764156, -2.450000000000000622 ) ) ;
#20368=DIRECTION ( 'NONE',  ( 1.000000000000000000, 4.440892098500622217E-16, 0.000000000000000000 ) ) ;
#20454=ORIENTED_EDGE ( 'NONE', *, *, #5850, .F. ) ;
#20472=EDGE_LOOP ( 'NONE', ( #11611, #23365, #17136 ) ) ;
#20473=FILL_AREA_STYLE_COLOUR ( '', #26342 ) ;
#20504=CARTESIAN_POINT ( 'NONE',  ( -4.000000000000003553, -6.938893903907228378E-15, 8.673617379884035472E-16 ) ) ;
#20507=DIRECTION ( 'NONE',  ( 1.000000000000000000, 4.440892098500622217E-16, 0.000000000000000000 ) ) ;
#20564=AXIS2_PLACEMENT_3D ( 'NONE', #19724, #15140, #3567 ) ;
#20566=CARTESIAN_POINT ( 'NONE',  ( 2.000000000000026201, 3.464101615137736623, 8.673617379884035472E-16 ) ) ;
#20624=SURFACE_SIDE_STYLE ('',( #4007 ) ) ;
#20662=DIRECTION ( 'NONE',  ( 1.000000000000000000, 4.440892098500622217E-16, 0.000000000000000000 ) ) ;
#20675=DIRECTION ( 'NONE',  ( -1.000000000000000000, -1.332267629550187651E-15, 0.000000000000000000 ) ) ;
#20708=CARTESIAN_POINT ( 'NONE',  ( 3.344563996438202569, 2.687817229851458212, -0.1586754815284793507 ) ) ;
#20736=DIRECTION ( 'NONE',  ( 1.000000000000000000, 4.440892098500622217E-16, 0.000000000000000000 ) ) ;
#20747=ORIENTED_EDGE ( 'NONE', *, *, #7573, .F. ) ;
#20791=DIRECTION ( 'NONE',  ( 1.000000000000000000, 4.440892098500622217E-16, 0.000000000000000000 ) ) ;
#20810=DIRECTION ( 'NONE',  ( 0.000000000000000000, 0.000000000000000000, -1.000000000000000000 ) ) ;
#20834=CARTESIAN_POINT ( 'NONE',  ( 3.999999999999980904, -2.309401076758567317, -2.092734410091829034 ) ) ;
#20903=ORIENTED_EDGE ( 'NONE', *, *, #8493, .T. ) ;
#20913=AXIS2_PLACEMENT_3D ( 'NONE', #27550, #9173, #22787 ) ;
#20919=CARTESIAN_POINT ( 'NONE',  ( 3.999999999999999112, 0.7862748000878193588, -0.03447227762756639030 ) ) ;
#20920=SHAPE_DEFINITION_REPRESENTATION ( #24215, #6235 ) ;
#20926=EDGE_CURVE ( 'NONE', #21764, #9008, #30051, .T. ) ;
#20954=CARTESIAN_POINT ( 'NONE',  ( 2.928571428571432378, 1.300546971703755312E-15, 1.700000000000000178 ) ) ;
#20957=STYLED_ITEM ( 'NONE', ( #15741 ), #6562 ) ;
#20967=FACE_OUTER_BOUND ( 'NONE', #7971, .T. ) ;
#21000=EDGE_CURVE ( 'NONE', #952, #3702, #2258, .T. ) ;
#21045=CARTESIAN_POINT ( 'NONE',  ( 3.345653888883660443, -2.687187980154745137, -0.1391502195351530802 ) ) ;
#21071=ORIENTED_EDGE ( 'NONE', *, *, #19136, .F. ) ;
#21098=EDGE_CURVE ( 'NONE', #952, #22117, #5083, .T. ) ;
#21120=CARTESIAN_POINT ( 'NONE',  ( -2.928571428571429713, -9.419004090963149730E-16, 2.549999999999998490 ) ) ;
#21264=AXIS2_PLACEMENT_3D ( 'NONE', #12579, #8600, #26810 ) ;
#21288=PLANE ( 'NONE',  #25626 ) ;
#21291=AXIS2_PLACEMENT_3D ( 'NONE', #4850, #6860, #9722 ) ;
#21424=ADVANCED_FACE ( 'NONE', ( #28358 ), #1289, .T. ) ;
#21445=ORIENTED_EDGE ( 'NONE', *, *, #7320, .F. ) ;
#21496=CIRCLE ( 'NONE', #565, 4.000000000000003553 ) ;
#21515=CARTESIAN_POINT ( 'NONE',  ( 0.000000000000000000, 0.000000000000000000, -2.424599999999998978 ) ) ;
#21585=AXIS2_PLACEMENT_3D ( 'NONE', #19957, #29329, #15821 ) ;
#21592=CARTESIAN_POINT ( 'NONE',  ( -1.660531772554310725, 3.660093687634845772, -2.450000000000005507 ) ) ;
#21593=CARTESIAN_POINT ( 'NONE',  ( -0.6543461111163949573, -4.241015250120828028, -0.1391502195351573268 ) ) ;
#21596=CARTESIAN_POINT ( 'NONE',  ( 4.000000000000003553, 2.309401076758525573, -2.092734410091829034 ) ) ;
#21600=ADVANCED_FACE ( 'NONE', ( #17886 ), #12870, .F. ) ;
#21635=CARTESIAN_POINT ( 'NONE',  ( 1.214306433183764966E-14, 4.618802153517016507, -2.092734410091829034 ) ) ;
#21641=CARTESIAN_POINT ( 'NONE',  ( 0.000000000000000000, 0.000000000000000000, -2.450000000000000178 ) ) ;
#21657=DIRECTION ( 'NONE',  ( 0.000000000000000000, 0.000000000000000000, -1.000000000000000000 ) ) ;
#21698=( NAMED_UNIT ( * ) SI_UNIT ( $, .STERADIAN. ) SOLID_ANGLE_UNIT ( ) );
#21700=EDGE_LOOP ( 'NONE', ( #25649, #21915, #4028, #1912, #19981, #8090 ) ) ;
#21711=EDGE_CURVE ( 'NONE', #21764, #17928, #26283, .T. ) ;
#21764=VERTEX_POINT ( 'NONE', #27368 ) ;
#21798=AXIS2_PLACEMENT_3D ( 'NONE', #3742, #27722, #20507 ) ;
#21816=DIRECTION ( 'NONE',  ( -1.000000000000000000, -4.440892098500622217E-16, 0.000000000000000000 ) ) ;
#21854=EDGE_LOOP ( 'NONE', ( #1882, #5124, #3943 ) ) ;
#21869=CIRCLE ( 'NONE', #9193, 2.100000000000002753 ) ;
#21899=CARTESIAN_POINT ( 'NONE',  ( -2.100000000000000977, -6.754115128641868940E-16, -2.450000000000000178 ) ) ;
#21904=ORIENTED_EDGE ( 'NONE', *, *, #7771, .T. ) ;
#21915=ORIENTED_EDGE ( 'NONE', *, *, #20270, .F. ) ;
#21926=DIRECTION ( 'NONE',  ( 0.000000000000000000, 0.000000000000000000, 1.000000000000000000 ) ) ;
#21928=FACE_OUTER_BOUND ( 'NONE', #18857, .T. ) ;
#22001=FACE_OUTER_BOUND ( 'NONE', #19469, .T. ) ;
#22034=DIRECTION ( 'NONE',  ( 0.000000000000000000, 0.000000000000000000, 1.000000000000000000 ) ) ;
#22073=CARTESIAN_POINT ( 'NONE',  ( 3.999999999999998224, 2.309401076758477167, -2.450000000000000178 ) ) ;
#22080=FACE_OUTER_BOUND ( 'NONE', #11590, .T. ) ;
#22096=DIRECTION ( 'NONE',  ( 0.000000000000000000, 0.000000000000000000, 1.000000000000000000 ) ) ;
#22099=ORIENTED_EDGE ( 'NONE', *, *, #19542, .F. ) ;
#22103=EDGE_CURVE ( 'NONE', #15438, #952, #1809, .T. ) ;
#22117=VERTEX_POINT ( 'NONE', #20050 ) ;
#22154=ORIENTED_EDGE ( 'NONE', *, *, #29958, .T. ) ;
#22164=CARTESIAN_POINT ( 'NONE',  ( -4.000000000000003553, 0.3904826640787941172, -2.138334675343480417E-15 ) ) ;
#22183=DIRECTION ( 'NONE',  ( 0.000000000000000000, 0.000000000000000000, 1.000000000000000000 ) ) ;
#22186=CARTESIAN_POINT ( 'NONE',  ( -7.806255641895631925E-14, -4.618802153517044928, -0.3572655899081716435 ) ) ;
#22203=EDGE_CURVE ( 'NONE', #4780, #13842, #20302, .T. ) ;
#22289=VECTOR ( 'NONE', #2169, 1000.000000000000000 ) ;
#22324=DIRECTION ( 'NONE',  ( -3.216245299353268764E-16, 1.000000000000000000, 0.000000000000000000 ) ) ;
#22485=PLANE ( 'NONE',  #20564 ) ;
#22529=ORIENTED_EDGE ( 'NONE', *, *, #26, .F. ) ;
#22560=CARTESIAN_POINT ( 'NONE',  ( 0.000000000000000000, 0.000000000000000000, -2.450000000000000622 ) ) ;
#22609=ORIENTED_EDGE ( 'NONE', *, *, #13526, .T. ) ;
#22636=DIRECTION ( 'NONE',  ( 1.000000000000000000, 4.440892098500622217E-16, 0.000000000000000000 ) ) ;
#22691=EDGE_LOOP ( 'NONE', ( #8243, #11032, #26639, #4130, #9485, #4731 ) ) ;
#22698=CARTESIAN_POINT ( 'NONE',  ( -7.806255641895631925E-14, -4.618802153517044928, -2.092734410091829034 ) ) ;
#22709=FACE_OUTER_BOUND ( 'NONE', #14345, .T. ) ;
#22771=LINE ( 'NONE', #22926, #24210 ) ;
#22787=DIRECTION ( 'NONE',  ( 1.000000000000000000, 4.440892098500622217E-16, 0.000000000000000000 ) ) ;
#22807=CARTESIAN_POINT ( 'NONE',  ( 4.000000000000000000, 0.000000000000000000, -2.450000000000000622 ) ) ;
#22907=DIRECTION ( 'NONE',  ( 0.000000000000000000, 0.000000000000000000, 1.000000000000000000 ) ) ;
#22916=EDGE_CURVE ( 'NONE', #28553, #5044, #23569, .T. ) ;
#22926=CARTESIAN_POINT ( 'NONE',  ( -4.000000000000005329, 2.309401076758490934, -2.450000000000000178 ) ) ;
#22935=( NAMED_UNIT ( * ) SI_UNIT ( $, .STERADIAN. ) SOLID_ANGLE_UNIT ( ) );
#22975=CARTESIAN_POINT ( 'NONE',  ( -4.000000000000010658, -2.309401076758525573, -2.092734410091829034 ) ) ;
#22980=CARTESIAN_POINT ( 'NONE',  ( 2.000000000000026201, 3.464101615137736623, -2.450000000000000622 ) ) ;
#23039=ADVANCED_FACE ( 'NONE', ( #21928 ), #12611, .F. ) ;
#23115=CIRCLE ( 'NONE', #17733, 2.928571428571432378 ) ;
#23189=CARTESIAN_POINT ( 'NONE',  ( 3.345653888883659555, -2.687187980154746025, -2.310849780464848013 ) ) ;
#23202=ORIENTED_EDGE ( 'NONE', *, *, #13526, .F. ) ;
#23325=CIRCLE ( 'NONE', #2888, 2.100000000000000977 ) ;
#23345=TOROIDAL_SURFACE ( 'NONE', #7278, 3.149999999999996358, 0.8500000000000000888 ) ;
#23365=ORIENTED_EDGE ( 'NONE', *, *, #3600, .F. ) ;
#23450=AXIS2_PLACEMENT_3D ( 'NONE', #24373, #7734, #17047 ) ;
#23458=ADVANCED_FACE ( 'NONE', ( #11969, #14560 ), #21288, .F. ) ;
#23499=ORIENTED_EDGE ( 'NONE', *, *, #25211, .T. ) ;
#23569=B_SPLINE_CURVE_WITH_KNOTS ( 'NONE', 3,
 ( #26074, #28240, #7296, #7589, #28395, #25921 ),
 .UNSPECIFIED., .F., .F.,
 ( 4, 2, 4 ),
 ( 0.006456566858647419180, 0.007625406818786685526, 0.008794246778925951871 ),
 .UNSPECIFIED. ) ;
#23606=ORIENTED_EDGE ( 'NONE', *, *, #14236, .T. ) ;
#23611=DIRECTION ( 'NONE',  ( 0.000000000000000000, 0.000000000000000000, 1.000000000000000000 ) ) ;
#23630=DIRECTION ( 'NONE',  ( 0.000000000000000000, 0.000000000000000000, 1.000000000000000000 ) ) ;
#23720=CONICAL_SURFACE ( 'NONE', #21264, 4.000000000000003553, 1.047197551196597853 ) ;
#23731=CARTESIAN_POINT ( 'NONE',  ( 1.318516776095786991, 3.857556137907067750, -2.450000000000006395 ) ) ;
#23789=VERTEX_POINT ( 'NONE', #29737 ) ;
#23805=CARTESIAN_POINT ( 'NONE',  ( -3.345653888883675542, 2.687187980154690514, -0.1391502195351382032 ) ) ;
#23889=EDGE_CURVE ( 'NONE', #6921, #28553, #4997, .T. ) ;
#23914=AXIS2_PLACEMENT_3D ( 'NONE', #18613, #25491, #6722 ) ;
#23922=VERTEX_POINT ( 'NONE', #13628 ) ;
#23925=VECTOR ( 'NONE', #4927, 1000.000000000000000 ) ;
#23990=ORIENTED_EDGE ( 'NONE', *, *, #12976, .T. ) ;
#23992=CARTESIAN_POINT ( 'NONE',  ( 0.000000000000000000, 0.000000000000000000, 0.000000000000000000 ) ) ;
#24010=ORIENTED_EDGE ( 'NONE', *, *, #409, .T. ) ;
#24049=CARTESIAN_POINT ( 'NONE',  ( -1.318516776095826071, -3.857556137907095284, -1.931970283426452982E-14 ) ) ;
#24084=CARTESIAN_POINT ( 'NONE',  ( -4.000000000000010658, -2.309401076758525573, -2.450000000000000178 ) ) ;
#24115=EDGE_LOOP ( 'NONE', ( #22529, #7208, #3237 ) ) ;
#24141=CARTESIAN_POINT ( 'NONE',  ( -4.000000000000010658, -2.309401076758525573, -2.450000000000000178 ) ) ;
#24144=EDGE_CURVE ( 'NONE', #28630, #23789, #28137, .T. ) ;
#24198=EDGE_LOOP ( 'NONE', ( #14942, #26334, #16161, #12440 ) ) ;
#24210=VECTOR ( 'NONE', #15877, 1000.000000000000000 ) ;
#24215=PRODUCT_DEFINITION_SHAPE ( 'NONE', 'NONE',  #4667 ) ;
#24242=STYLED_ITEM ( 'NONE', ( #4625 ), #11686 ) ;
#24314=CARTESIAN_POINT ( 'NONE',  ( -4.000000000000003553, -6.938893903907228378E-15, 8.673617379884035472E-16 ) ) ;
#24322=EDGE_LOOP ( 'NONE', ( #16228, #3410, #958, #10152 ) ) ;
#24373=CARTESIAN_POINT ( 'NONE',  ( 0.000000000000000000, 0.000000000000000000, -2.450000000000000178 ) ) ;
#24395=EDGE_CURVE ( 'NONE', #23922, #19336, #22771, .T. ) ;
#24404=B_SPLINE_CURVE_WITH_KNOTS ( 'NONE', 3,
 ( #22186, #21593, #24049, #10586 ),
 .UNSPECIFIED., .F., .F.,
 ( 4, 4 ),
 ( 2.380737582341110265E-07, 0.002336974151641603697 ),
 .UNSPECIFIED. ) ;
#24444=ADVANCED_FACE ( 'NONE', ( #27679 ), #11023, .F. ) ;
#24499=ORIENTED_EDGE ( 'NONE', *, *, #409, .F. ) ;
#24594=EDGE_CURVE ( 'NONE', #3702, #9337, #14819, .T. ) ;
#24648=FACE_OUTER_BOUND ( 'NONE', #8996, .T. ) ;
#24670=DIRECTION ( 'NONE',  ( 0.000000000000000000, 0.000000000000000000, 1.000000000000000000 ) ) ;
#24724=AXIS2_PLACEMENT_3D ( 'NONE', #26763, #10092, #15271 ) ;
#24788=ORIENTED_EDGE ( 'NONE', *, *, #13925, .T. ) ;
#24791=CARTESIAN_POINT ( 'NONE',  ( 0.000000000000000000, 0.000000000000000000, -2.450000000000000178 ) ) ;
#24794=CARTESIAN_POINT ( 'NONE',  ( 0.000000000000000000, 0.000000000000000000, 1.699999999999996625 ) ) ;
#24806=ORIENTED_EDGE ( 'NONE', *, *, #22103, .F. ) ;
#24843=B_SPLINE_CURVE_WITH_KNOTS ( 'NONE', 3,
 ( #13866, #23805, #2302, #2904 ),
 .UNSPECIFIED., .F., .F.,
 ( 4, 4 ),
 ( 2.380737581560122065E-07, 0.002336974151641542981 ),
 .UNSPECIFIED. ) ;
#24879=FACE_OUTER_BOUND ( 'NONE', #25435, .T. ) ;
#24945=DIRECTION ( 'NONE',  ( -1.000000000000000000, 4.884981308350688778E-15, 0.000000000000000000 ) ) ;
#25092=CARTESIAN_POINT ( 'NONE',  ( 4.000000000000000000, -1.933795701539638534, -2.201162342337696476 ) ) ;
#25114=CARTESIAN_POINT ( 'NONE',  ( 0.000000000000000000, 0.000000000000000000, 9.480888224575629408 ) ) ;
#25116=LINE ( 'NONE', #13054, #20178 ) ;
#25211=EDGE_CURVE ( 'NONE', #12251, #27629, #4243, .T. ) ;
#25218=ADVANCED_FACE ( 'NONE', ( #11712 ), #25467, .T. ) ;
#25225=ORIENTED_EDGE ( 'NONE', *, *, #27970, .F. ) ;
#25325=DIRECTION ( 'NONE',  ( 1.000000000000000000, 4.440892098500622217E-16, 0.000000000000000000 ) ) ;
#25410=CARTESIAN_POINT ( 'NONE',  ( 2.500000000000002665, 1.416384724411995397E-15, -2.424599999999998978 ) ) ;
#25435=EDGE_LOOP ( 'NONE', ( #18949, #21445, #11144 ) ) ;
#25467=CYLINDRICAL_SURFACE ( 'NONE', #16429, 4.000000000000001776 ) ;
#25490=ADVANCED_FACE ( 'NONE', ( #24648 ), #1357, .T. ) ;
#25491=DIRECTION ( 'NONE',  ( 0.000000000000000000, 0.000000000000000000, -1.000000000000000000 ) ) ;
#25492=DIRECTION ( 'NONE',  ( -1.000000000000000000, -4.440892098500623203E-16, 0.000000000000000000 ) ) ;
#25600=AXIS2_PLACEMENT_3D ( 'NONE', #28158, #25986, #501 ) ;
#25602=VERTEX_POINT ( 'NONE', #20954 ) ;
#25617=B_SPLINE_CURVE_WITH_KNOTS ( 'NONE', 3,
 ( #9184, #18811, #14219, #13916 ),
 .UNSPECIFIED., .F., .F.,
 ( 4, 4 ),
 ( 2.380737582341341346E-07, 0.002336974151641586783 ),
 .UNSPECIFIED. ) ;
#25626=AXIS2_PLACEMENT_3D ( 'NONE', #398, #14408, #28052 ) ;
#25627=CARTESIAN_POINT ( 'NONE',  ( 2.100000000000002753, 9.325873406851319278E-16, 1.700000000000000178 ) ) ;
#25629=CARTESIAN_POINT ( 'NONE',  ( 2.000000000000008882, -3.464101615137750390, -2.450000000000000622 ) ) ;
#25649=ORIENTED_EDGE ( 'NONE', *, *, #14236, .F. ) ;
#25650=CARTESIAN_POINT ( 'NONE',  ( -3.344563996438228770, -2.687817229851498180, -0.1586754815285055242 ) ) ;
#25687=LINE ( 'NONE', #7225, #23925 ) ;
#25759=CIRCLE ( 'NONE', #11603, 2.100000000000002753 ) ;
#25766=CIRCLE ( 'NONE', #19430, 2.500000000000002665 ) ;
#25770=ORIENTED_EDGE ( 'NONE', *, *, #24594, .T. ) ;
#25808=CARTESIAN_POINT ( 'NONE',  ( 0.6554360035617690095, -4.240386000424094526, -2.291324518471481220 ) ) ;
#25862=AXIS2_PLACEMENT_3D ( 'NONE', #10466, #21926, #1041 ) ;
#25890=B_SPLINE_CURVE_WITH_KNOTS ( 'NONE', 3,
 ( #10752, #29584, #6331, #8454, #1916, #20504 ),
 .UNSPECIFIED., .F., .F.,
 ( 4, 2, 4 ),
 ( 0.004120275011746851387, 0.005288420935197119671, 0.006456566858647387087 ),
 .UNSPECIFIED. ) ;
#25921=CARTESIAN_POINT ( 'NONE',  ( 4.000000000000003553, 2.309401076758525573, -2.092734410091829034 ) ) ;
#25940=DIRECTION ( 'NONE',  ( 1.000000000000000000, 4.440892098500622217E-16, 0.000000000000000000 ) ) ;
#25947=CARTESIAN_POINT ( 'NONE',  ( 0.000000000000000000, 0.000000000000000000, -2.144516984716112518 ) ) ;
#25970=EDGE_LOOP ( 'NONE', ( #24788, #15782, #15718, #13228, #16757, #2876 ) ) ;
#25986=DIRECTION ( 'NONE',  ( 0.000000000000000000, 0.000000000000000000, -1.000000000000000000 ) ) ;
#25999=FILL_AREA_STYLE ('',( #16676 ) ) ;
#26026=CARTESIAN_POINT ( 'NONE',  ( 0.6543461111163458854, 4.241015250120808489, -2.310849780464859560 ) ) ;
#26074=CARTESIAN_POINT ( 'NONE',  ( 4.000000000000000000, 0.000000000000000000, -2.450000000000000622 ) ) ;
#26108=EDGE_CURVE ( 'NONE', #29328, #27629, #12070, .T. ) ;
#26117=VERTEX_POINT ( 'NONE', #15590 ) ;
#26283=LINE ( 'NONE', #12516, #15883 ) ;
#26289=PLANE ( 'NONE',  #7555 ) ;
#26334=ORIENTED_EDGE ( 'NONE', *, *, #12799, .T. ) ;
#26342=COLOUR_RGB ( '', 0.72549020, 0.75294118, 0.79215686) ;
#26349=AXIS2_PLACEMENT_3D ( 'NONE', #9206, #20810, #16084 ) ;
#26376=CYLINDRICAL_SURFACE ( 'NONE', #25862, 2.928571428571432378 ) ;
#26383=CARTESIAN_POINT ( 'NONE',  ( -2.000000000000008882, 3.464101615137750390, -2.450000000000000622 ) ) ;
#26386=ORIENTED_EDGE ( 'NONE', *, *, #783, .T. ) ;
#26416=ORIENTED_EDGE ( 'NONE', *, *, #19365, .T. ) ;
#26437=CARTESIAN_POINT ( 'NONE',  ( 1.318516776095787435, 3.857556137907067750, 4.982961509259709006E-15 ) ) ;
#26442=DIRECTION ( 'NONE',  ( -1.000000000000000000, -4.440892098500622217E-16, 0.000000000000000000 ) ) ;
#26530=DIRECTION ( 'NONE',  ( 0.000000000000000000, 0.000000000000000000, 1.000000000000000000 ) ) ;
#26531=CARTESIAN_POINT ( 'NONE',  ( -4.000000000000001776, 2.309401076758532678, -2.092734410091829034 ) ) ;
#26535=B_SPLINE_CURVE_WITH_KNOTS ( 'NONE', 3,
 ( #9553, #11996, #714, #17042, #9703, #16742 ),
 .UNSPECIFIED., .F., .F.,
 ( 4, 2, 4 ),
 ( 0.006456566858647387955, 0.007625406818786661239, 0.008794246778925934524 ),
 .UNSPECIFIED. ) ;
#26542=CARTESIAN_POINT ( 'NONE',  ( 3.999999999999998224, 2.309401076758477167, -2.450000000000000178 ) ) ;
#26583=DIRECTION ( 'NONE',  ( 0.8191520442889902442, 4.640937770007129962E-16, -0.5735764363510482688 ) ) ;
#26596=ORIENTED_EDGE ( 'NONE', *, *, #26108, .F. ) ;
#26632=CARTESIAN_POINT ( 'NONE',  ( 0.000000000000000000, 0.000000000000000000, -2.450000000000000622 ) ) ;
#26639=ORIENTED_EDGE ( 'NONE', *, *, #21098, .T. ) ;
#26642=CARTESIAN_POINT ( 'NONE',  ( 1.214306433183764966E-14, 4.618802153517016507, -0.3572655899081716435 ) ) ;
#26653=LINE ( 'NONE', #21899, #17121 ) ;
#26671=ADVANCED_FACE ( 'NONE', ( #14643 ), #5771, .T. ) ;
#26681=AXIS2_PLACEMENT_3D ( 'NONE', #8340, #19773, #17340 ) ;
#26712=B_SPLINE_CURVE_WITH_KNOTS ( 'NONE', 3,
 ( #9680, #16717, #18846, #12278, #694, #21596 ),
 .UNSPECIFIED., .F., .F.,
 ( 4, 2, 4 ),
 ( 0.002336974151641584615, 0.003500975885716457563, 0.004664977619791330077 ),
 .UNSPECIFIED. ) ;
#26763=CARTESIAN_POINT ( 'NONE',  ( 0.000000000000000000, 0.000000000000000000, -2.424599999999998978 ) ) ;
#26791=AXIS2_PLACEMENT_3D ( 'NONE', #26632, #22034, #5712 ) ;
#26807=ORIENTED_EDGE ( 'NONE', *, *, #783, .F. ) ;
#26810=DIRECTION ( 'NONE',  ( -1.000000000000000000, -4.440892098500622217E-16, 0.000000000000000000 ) ) ;
#26840=FACE_OUTER_BOUND ( 'NONE', #404, .T. ) ;
#26865=VERTEX_POINT ( 'NONE', #1690 ) ;
#26905=CARTESIAN_POINT ( 'NONE',  ( 1.214306433183764966E-14, 4.618802153517016507, -0.3572655899081716435 ) ) ;
#26998=CARTESIAN_POINT ( 'NONE',  ( 4.000000000000000000, 1.776356839400248887E-15, 1.699999999999996625 ) ) ;
#27010=ORIENTED_EDGE ( 'NONE', *, *, #2111, .F. ) ;
#27019=CARTESIAN_POINT ( 'NONE',  ( 0.000000000000000000, 0.000000000000000000, -2.424599999999998978 ) ) ;
#27045=EDGE_CURVE ( 'NONE', #5490, #18869, #906, .T. ) ;
#27061=PLANE ( 'NONE',  #9207 ) ;
#27083=CARTESIAN_POINT ( 'NONE',  ( -4.000000000000005329, 2.309401076758490934, -0.3572655899081616515 ) ) ;
#27135=DIRECTION ( 'NONE',  ( 0.000000000000000000, 0.000000000000000000, 1.000000000000000000 ) ) ;
#27235=DIRECTION ( 'NONE',  ( 0.000000000000000000, 0.000000000000000000, -1.000000000000000000 ) ) ;
#27238=ORIENTED_EDGE ( 'NONE', *, *, #5119, .F. ) ;
#27241=EDGE_LOOP ( 'NONE', ( #23202, #14447, #5027, #15676 ) ) ;
#27266=CARTESIAN_POINT ( 'NONE',  ( 0.000000000000000000, 0.000000000000000000, 19.04999999999997229 ) ) ;
#27276=VECTOR ( 'NONE', #22096, 1000.000000000000000 ) ;
#27325=EDGE_CURVE ( 'NONE', #23789, #28630, #25766, .T. ) ;
#27348=ORIENTED_EDGE ( 'NONE', *, *, #3072, .T. ) ;
#27368=CARTESIAN_POINT ( 'NONE',  ( 2.099999999999999645, 9.325873406851305473E-16, -2.144516984716112518 ) ) ;
#27372=ORIENTED_EDGE ( 'NONE', *, *, #19029, .F. ) ;
#27382=ORIENTED_EDGE ( 'NONE', *, *, #10991, .F. ) ;
#27518=CARTESIAN_POINT ( 'NONE',  ( -2.500000000000000444, -8.040613248383173881E-16, -2.450000000000000622 ) ) ;
#27550=CARTESIAN_POINT ( 'NONE',  ( 0.000000000000000000, 0.000000000000000000, 1.700000000000000178 ) ) ;
#27629=VERTEX_POINT ( 'NONE', #12115 ) ;
#27652=AXIS2_PLACEMENT_3D ( 'NONE', #19859, #15272, #29070 ) ;
#27679=FACE_OUTER_BOUND ( 'NONE', #28290, .T. ) ;
#27700=CARTESIAN_POINT ( 'NONE',  ( -2.000000000000008882, 3.464101615137750390, 0.000000000000000000 ) ) ;
#27722=DIRECTION ( 'NONE',  ( 0.000000000000000000, 0.000000000000000000, 1.000000000000000000 ) ) ;
#27759=ORIENTED_EDGE ( 'NONE', *, *, #27045, .F. ) ;
#27793=CARTESIAN_POINT ( 'NONE',  ( -2.500000000000002665, -8.040613248383180784E-16, 19.04999999999997229 ) ) ;
#27855=PRODUCT_DEFINITION_CONTEXT ( 'detailed design', #19802, 'design' ) ;
#27875=CARTESIAN_POINT ( 'NONE',  ( 3.999999999999980904, -2.309401076758567317, -2.092734410091829034 ) ) ;
#27932=ADVANCED_FACE ( 'NONE', ( #19582 ), #4838, .T. ) ;
#27942=CARTESIAN_POINT ( 'NONE',  ( 1.214306433183764966E-14, 4.618802153517016507, -0.3572655899081716435 ) ) ;
#27957=CARTESIAN_POINT ( 'NONE',  ( 3.999999999999980904, -2.309401076758567317, -0.3572655899081716435 ) ) ;
#27970=EDGE_CURVE ( 'NONE', #8103, #25602, #3872, .T. ) ;
#27991=CARTESIAN_POINT ( 'NONE',  ( 3.999999999999999112, 1.935983797701081643, -0.2494693066162320116 ) ) ;
#28013=( LENGTH_UNIT ( ) NAMED_UNIT ( * ) SI_UNIT ( .MILLI., .METRE. ) );
#28030=AXIS2_PLACEMENT_3D ( 'NONE', #18538, #28196, #15940 ) ;
#28036=CARTESIAN_POINT ( 'NONE',  ( 0.000000000000000000, 0.000000000000000000, -2.450000000000000622 ) ) ;
#28052=DIRECTION ( 'NONE',  ( -1.000000000000000000, -4.440892098500622217E-16, -0.000000000000000000 ) ) ;
#28089=ORIENTED_EDGE ( 'NONE', *, *, #12552, .F. ) ;
#28137=CIRCLE ( 'NONE', #27652, 2.500000000000002665 ) ;
#28158=CARTESIAN_POINT ( 'NONE',  ( 0.000000000000000000, 0.000000000000000000, 0.000000000000000000 ) ) ;
#28163=EDGE_LOOP ( 'NONE', ( #25225, #22609, #8489, #10853 ) ) ;
#28196=DIRECTION ( 'NONE',  ( -0.5000000000000027756, 0.8660254037844370423, 0.000000000000000000 ) ) ;
#28240=CARTESIAN_POINT ( 'NONE',  ( 4.000000000000000000, 0.3904826640788077730, -2.450000000000000622 ) ) ;
#28245=FACE_OUTER_BOUND ( 'NONE', #20030, .T. ) ;
#28290=EDGE_LOOP ( 'NONE', ( #5638, #2311, #23990, #14727 ) ) ;
#28358=FACE_OUTER_BOUND ( 'NONE', #24115, .T. ) ;
#28395=CARTESIAN_POINT ( 'NONE',  ( 3.999999999999999112, 1.935983797701081643, -2.200530693383769609 ) ) ;
#28441=ORIENTED_EDGE ( 'NONE', *, *, #5714, .T. ) ;
#28452=ADVANCED_FACE ( 'NONE', ( #8093 ), #27061, .T. ) ;
#28553=VERTEX_POINT ( 'NONE', #13729 ) ;
#28573=FACE_OUTER_BOUND ( 'NONE', #24322, .T. ) ;
#28603=DIRECTION ( 'NONE',  ( 0.000000000000000000, 0.000000000000000000, 1.000000000000000000 ) ) ;
#28611=SURFACE_STYLE_FILL_AREA ( #25999 ) ;
#28630=VERTEX_POINT ( 'NONE', #27518 ) ;
#28636=APPLICATION_CONTEXT ( 'automotive_design' ) ;
#28651=CARTESIAN_POINT ( 'NONE',  ( 1.214306433183764966E-14, 4.618802153517016507, -2.092734410091829034 ) ) ;
#28662=DIRECTION ( 'NONE',  ( 0.000000000000000000, 0.000000000000000000, 1.000000000000000000 ) ) ;
#28692=CARTESIAN_POINT ( 'NONE',  ( -2.681483223904232549, 3.070647092368427256, -2.450000000000005063 ) ) ;
#28794=ORIENTED_EDGE ( 'NONE', *, *, #10347, .T. ) ;
#28797=CONICAL_SURFACE ( 'NONE', #986, 4.000000000000003553, 1.047197551196597853 ) ;
#28814=CARTESIAN_POINT ( 'NONE',  ( -1.321505333908961966, 3.855830693249140406, -0.03421028094653050244 ) ) ;
#28940=( LENGTH_UNIT ( ) NAMED_UNIT ( * ) SI_UNIT ( .MILLI., .METRE. ) );
#28960=CARTESIAN_POINT ( 'NONE',  ( -2.000000000000032863, -3.464101615137743728, 8.673617379884035472E-16 ) ) ;
#28986=DIRECTION ( 'NONE',  ( 0.000000000000000000, 0.000000000000000000, -1.000000000000000000 ) ) ;
#29035=VERTEX_POINT ( 'NONE', #29810 ) ;
#29053=CARTESIAN_POINT ( 'NONE',  ( 0.000000000000000000, 0.000000000000000000, -2.450000000000000622 ) ) ;
#29070=DIRECTION ( 'NONE',  ( -1.000000000000000000, -4.440892098500622217E-16, 0.000000000000000000 ) ) ;
#29079=ORIENTED_EDGE ( 'NONE', *, *, #7573, .T. ) ;
#29087=ORIENTED_EDGE ( 'NONE', *, *, #5125, .T. ) ;
#29094=TOROIDAL_SURFACE ( 'NONE', #15872, 3.149999999999996358, 0.8500000000000000888 ) ;
#29155=CIRCLE ( 'NONE', #24724, 2.500000000000002665 ) ;
#29234=CARTESIAN_POINT ( 'NONE',  ( -4.000000000000005329, 1.935983797701048559, -0.2494693066162272932 ) ) ;
#29257=ADVANCED_FACE ( 'NONE', ( #10627 ), #26376, .F. ) ;
#29323=DIRECTION ( 'NONE',  ( 1.000000000000000000, 4.440892098500622217E-16, 0.000000000000000000 ) ) ;
#29328=VERTEX_POINT ( 'NONE', #26998 ) ;
#29329=DIRECTION ( 'NONE',  ( 0.000000000000000000, 0.000000000000000000, 1.000000000000000000 ) ) ;
#29399=DIRECTION ( 'NONE',  ( 0.000000000000000000, 0.000000000000000000, 1.000000000000000000 ) ) ;
#29412=CARTESIAN_POINT ( 'NONE',  ( 0.000000000000000000, 0.000000000000000000, 0.000000000000000000 ) ) ;
#29434=ORIENTED_EDGE ( 'NONE', *, *, #3072, .F. ) ;
#29541=ORIENTED_EDGE ( 'NONE', *, *, #17176, .F. ) ;
#29550=CARTESIAN_POINT ( 'NONE',  ( -4.000000000000005329, 0.7862748000877981536, -0.03447227762756752828 ) ) ;
#29584=CARTESIAN_POINT ( 'NONE',  ( -4.000000000000003553, -1.933795701539603895, -0.2488376576622973180 ) ) ;
#29667=ORIENTED_EDGE ( 'NONE', *, *, #14990, .F. ) ;
#29675=AXIS2_PLACEMENT_3D ( 'NONE', #22073, #3606, #19470 ) ;
#29677=FACE_OUTER_BOUND ( 'NONE', #7522, .T. ) ;
#29705=( NAMED_UNIT ( * ) PLANE_ANGLE_UNIT ( ) SI_UNIT ( $, .RADIAN. ) );
#29737=CARTESIAN_POINT ( 'NONE',  ( 2.500000000000000444, 1.110223024625155752E-15, -2.450000000000000622 ) ) ;
#29810=CARTESIAN_POINT ( 'NONE',  ( 4.000000000000003553, 2.309401076758525573, -0.3572655899081716435 ) ) ;
#29919=VERTEX_POINT ( 'NONE', #25627 ) ;
#29938=VERTEX_POINT ( 'NONE', #9739 ) ;
#29958=EDGE_CURVE ( 'NONE', #19336, #2732, #24843, .T. ) ;
#30008=CIRCLE ( 'NONE', #5582, 4.000000000000003553 ) ;
#30050=FACE_OUTER_BOUND ( 'NONE', #17501, .T. ) ;
#30051=CIRCLE ( 'NONE', #781, 2.100000000000000977 ) ;
#30176=CARTESIAN_POINT ( 'NONE',  ( 0.000000000000000000, 0.000000000000000000, 2.550000000000000266 ) ) ;
#30199=CARTESIAN_POINT ( 'NONE',  ( 0.000000000000000000, 0.000000000000000000, -2.450000000000000178 ) ) ;
#30237=DIRECTION ( 'NONE',  ( -1.000000000000000000, -4.440892098500622217E-16, -0.000000000000000000 ) ) ;
#30242=ORIENTED_EDGE ( 'NONE', *, *, #13412, .T. ) ;
ENDSEC;
END-ISO-10303-21;
